ISO-10303-21;
HEADER;
FILE_DESCRIPTION (('STEP AP214'),
    '1' );
FILE_NAME ('hex thin nut chamfered gradeab_iso_ISO - 4035 - M10 - N.step',
    '2026-09-30T16:28:02',
    ( '' ),
    ( '' ),
    'SwSTEP 2.0',
    'SolidWorks 2026',
    '' );
FILE_SCHEMA (( 'AUTOMOTIVE_DESIGN' ));
ENDSEC;

DATA;
#51=CARTESIAN_POINT ( 'NONE',  ( 4.000000000000019540, 6.928203230275512325, 0.000000000000000000 ) ) ;
#53=AXIS2_PLACEMENT_3D ( 'NONE', #5832, #6438, #24451 ) ;
#101=EDGE_CURVE ( 'NONE', #2266, #29239, #23530, .T. ) ;
#138=EDGE_CURVE ( 'NONE', #19707, #18049, #20216, .T. ) ;
#145=CARTESIAN_POINT ( 'NONE',  ( -2.644994884459112683, 7.710515798486374806, -0.08224679563972035756 ) ) ;
#202=CARTESIAN_POINT ( 'NONE',  ( 1.313474075707222521, 8.479269695850875976, -0.3167204509598505746 ) ) ;
#211=ORIENTED_EDGE ( 'NONE', *, *, #18755, .T. ) ;
#268=ADVANCED_FACE ( 'NONE', ( #28096 ), #13304, .T. ) ;
#304=CARTESIAN_POINT ( 'NONE',  ( 0.000000000000000000, 0.000000000000000000, -0.5251556536572770106 ) ) ;
#323=VECTOR ( 'NONE', #10436, 1000.000000000000000 ) ;
#328=CARTESIAN_POINT ( 'NONE',  ( 4.680456609903983711, 6.535341423375600201, -4.983111142572226981 ) ) ;
#337=DIRECTION ( 'NONE',  ( 0.000000000000000000, 0.000000000000000000, 1.000000000000000000 ) ) ;
#347=CARTESIAN_POINT ( 'NONE',  ( 0.000000000000000000, 0.000000000000000000, -25.03750572909317285 ) ) ;
#401=CARTESIAN_POINT ( 'NONE',  ( 0.000000000000000000, 0.000000000000000000, -5.000000000000000888 ) ) ;
#445=CARTESIAN_POINT ( 'NONE',  ( -1.310872448937995705, 8.480771745766411129, -0.3173508448886640521 ) ) ;
#496=( GEOMETRIC_REPRESENTATION_CONTEXT ( 3 ) GLOBAL_UNCERTAINTY_ASSIGNED_CONTEXT ( ( #4915 ) ) GLOBAL_UNIT_ASSIGNED_CONTEXT ( ( #25066, #15887, #27085 ) ) REPRESENTATION_CONTEXT ( 'NONE', 'WORKASPACE' ) );
#498=FACE_OUTER_BOUND ( 'NONE', #5684, .T. ) ;
#515=AXIS2_PLACEMENT_3D ( 'NONE', #15266, #13594, #10844 ) ;
#540=CARTESIAN_POINT ( 'NONE',  ( 1.310872448937984602, -8.480771745766441327, -0.3173508448886784294 ) ) ;
#551=FACE_OUTER_BOUND ( 'NONE', #15661, .T. ) ;
#570=VERTEX_POINT ( 'NONE', #8354 ) ;
#634=CARTESIAN_POINT ( 'NONE',  ( -5.000000000000006217, -1.608122649676636551E-15, -25.03750572909317285 ) ) ;
#639=CARTESIAN_POINT ( 'NONE',  ( 0.000000000000000000, 0.000000000000000000, -5.000000000000000888 ) ) ;
#650=CARTESIAN_POINT ( 'NONE',  ( -8.000000000000000000, 4.618802153517001408, -0.7145311798163294092 ) ) ;
#678=CARTESIAN_POINT ( 'NONE',  ( 2.309976723937608778, -7.903938623646900474, -0.1306530452038287271 ) ) ;
#761=EDGE_LOOP ( 'NONE', ( #18408, #5576, #23225, #4103 ) ) ;
#832=CARTESIAN_POINT ( 'NONE',  ( -8.000000000000003553, -4.618802153517037823, -0.7145311798163362926 ) ) ;
#869=SURFACE_SIDE_STYLE ('',( #21768 ) ) ;
#887=VERTEX_POINT ( 'NONE', #29093 ) ;
#922=ORIENTED_EDGE ( 'NONE', *, *, #22458, .F. ) ;
#942=DIRECTION ( 'NONE',  ( 1.000000000000000000, 4.440892098500622217E-16, 0.000000000000000000 ) ) ;
#945=DIRECTION ( 'NONE',  ( 0.000000000000000000, 0.000000000000000000, -1.000000000000000000 ) ) ;
#949=CARTESIAN_POINT ( 'NONE',  ( -6.686525924292797463, 5.377136764700167326, -0.3167204509598451900 ) ) ;
#953=VECTOR ( 'NONE', #9784, 999.9999999999998863 ) ;
#971=ORIENTED_EDGE ( 'NONE', *, *, #28242, .T. ) ;
#989=CARTESIAN_POINT ( 'NONE',  ( 3.319543390096043378, -7.321065037175453760, -0.01688885742778342344 ) ) ;
#1047=DIRECTION ( 'NONE',  ( 0.000000000000000000, 0.000000000000000000, 1.000000000000000000 ) ) ;
#1138=CARTESIAN_POINT ( 'NONE',  ( -4.000000000000008882, 6.928203230275508773, -5.000000000000000888 ) ) ;
#1175=ORIENTED_EDGE ( 'NONE', *, *, #14689, .F. ) ;
#1184=CARTESIAN_POINT ( 'NONE',  ( 4.000000000000019540, 6.928203230275512325, -5.000000000000000888 ) ) ;
#1253=CARTESIAN_POINT ( 'NONE',  ( 7.345652830558766055, -4.996589667937400669, -4.503584543331195178 ) ) ;
#1308=CIRCLE ( 'NONE', #27647, 5.000000000000005329 ) ;
#1320=CARTESIAN_POINT ( 'NONE',  ( -2.645508037661914003, -7.710219529346629130, -0.06809871960544379432 ) ) ;
#1331=AXIS2_PLACEMENT_3D ( 'NONE', #11597, #23666, #18635 ) ;
#1337=DIRECTION ( 'NONE',  ( 0.000000000000000000, 0.000000000000000000, 1.000000000000000000 ) ) ;
#1339=CARTESIAN_POINT ( 'NONE',  ( -15.99999999999998224, -1.561251128379126385E-14, 0.000000000000000000 ) ) ;
#1424=VERTEX_POINT ( 'NONE', #27774 ) ;
#1438=CARTESIAN_POINT ( 'NONE',  ( -8.000000000000003553, -4.618802153517037823, -4.285468820183664818 ) ) ;
#1453=B_SPLINE_CURVE_WITH_KNOTS ( 'NONE', 3,
 ( #650, #9935, #949, #19247, #10237, #17262 ),
 .UNSPECIFIED., .F., .F.,
 ( 4, 2, 4 ),
 ( 2.380731629582120260E-07, 0.002336973833157553367, 0.004673709593152147908 ),
 .UNSPECIFIED. ) ;
#1482=CARTESIAN_POINT ( 'NONE',  ( 8.000000000000000000, -4.618802153517027165, -0.7145311798163362926 ) ) ;
#1518=APPLICATION_CONTEXT ( 'automotive_design' ) ;
#1519=CARTESIAN_POINT ( 'NONE',  ( -7.999999999999998224, 1.572549600175610962, -0.06894455525513019933 ) ) ;
#1528=CARTESIAN_POINT ( 'NONE',  ( -8.000000000000003553, -4.618802153517037823, -4.285468820183664818 ) ) ;
#1549=EDGE_CURVE ( 'NONE', #887, #12491, #24359, .T. ) ;
#1596=UNCERTAINTY_MEASURE_WITH_UNIT (LENGTH_MEASURE( 1.000000000000000082E-05 ), #3021, 'distance_accuracy_value', 'NONE');
#1634=CARTESIAN_POINT ( 'NONE',  ( 5.354491962338135735, -6.146186931204433712, -0.06809871960544290614 ) ) ;
#1645=FACE_BOUND ( 'NONE', #6745, .T. ) ;
#1679=VERTEX_POINT ( 'NONE', #11535 ) ;
#1714=B_SPLINE_CURVE_WITH_KNOTS ( 'NONE', 3,
 ( #13109, #1845, #27043, #13409, #17982, #22735 ),
 .UNSPECIFIED., .F., .F.,
 ( 4, 2, 4 ),
 ( 0.008240550023493518894, 0.01057684187039405199, 0.01291313371729458682 ),
 .UNSPECIFIED. ) ;
#1816=ORIENTED_EDGE ( 'NONE', *, *, #26363, .T. ) ;
#1835=MANIFOLD_SOLID_BREP ( 'EndChamfer', #26307 ) ;
#1839=DIRECTION ( 'NONE',  ( -1.000000000000000000, -4.440892098500622217E-16, 0.000000000000000000 ) ) ;
#1845=CARTESIAN_POINT ( 'NONE',  ( -7.999999999999996447, -3.867591403079199353, -0.4976753153245889738 ) ) ;
#1934=ADVANCED_FACE ( 'NONE', ( #13353 ), #25265, .T. ) ;
#2003=DIRECTION ( 'NONE',  ( -1.000000000000000000, -4.440892098500622217E-16, 0.000000000000000000 ) ) ;
#2037=FILL_AREA_STYLE ('',( #10716 ) ) ;
#2109=ADVANCED_FACE ( 'NONE', ( #9360 ), #9509, .F. ) ;
#2115=CARTESIAN_POINT ( 'NONE',  ( -4.000000000000008882, 6.928203230275508773, -5.000000000000000888 ) ) ;
#2130=DIRECTION ( 'NONE',  ( 0.5000000000000014433, -0.8660254037844378194, 0.000000000000000000 ) ) ;
#2145=ADVANCED_FACE ( 'NONE', ( #4797 ), #25167, .T. ) ;
#2266=VERTEX_POINT ( 'NONE', #26327 ) ;
#2282=EDGE_LOOP ( 'NONE', ( #11648, #19219, #5264, #14423 ) ) ;
#2300=DIRECTION ( 'NONE',  ( 0.000000000000000000, 0.000000000000000000, 1.000000000000000000 ) ) ;
#2310=EDGE_CURVE ( 'NONE', #887, #16400, #19794, .T. ) ;
#2314=EDGE_CURVE ( 'NONE', #15020, #15488, #14298, .T. ) ;
#2459=CARTESIAN_POINT ( 'NONE',  ( 0.000000000000000000, 0.000000000000000000, 0.000000000000000000 ) ) ;
#2551=ORIENTED_EDGE ( 'NONE', *, *, #27803, .F. ) ;
#2576=EDGE_LOOP ( 'NONE', ( #27818, #13186, #3069, #25362 ) ) ;
#2641=AXIS2_PLACEMENT_3D ( 'NONE', #10040, #12327, #10194 ) ;
#2791=CARTESIAN_POINT ( 'NONE',  ( -8.000000000000003553, -4.618802153517028941, -5.000000000000000888 ) ) ;
#2796=B_SPLINE_CURVE_WITH_KNOTS ( 'NONE', 3,
 ( #15773, #25099, #13485, #11346, #24962, #29892 ),
 .UNSPECIFIED., .F., .F.,
 ( 4, 2, 4 ),
 ( 0.01291313371729459203, 0.01525081363757311605, 0.01758849355785164006 ),
 .UNSPECIFIED. ) ;
#2832=CIRCLE ( 'NONE', #11552, 5.000000000000006217 ) ;
#2862=EDGE_LOOP ( 'NONE', ( #22736, #7896, #25769, #21484, #4484, #9143 ) ) ;
#2881=DIRECTION ( 'NONE',  ( 0.000000000000000000, 0.000000000000000000, 1.000000000000000000 ) ) ;
#2887=ADVANCED_FACE ( 'NONE', ( #498 ), #18904, .T. ) ;
#2892=CARTESIAN_POINT ( 'NONE',  ( 0.000000000000000000, 0.000000000000000000, 0.000000000000000000 ) ) ;
#2894=CARTESIAN_POINT ( 'NONE',  ( -8.000000000000003553, -4.618802153517037823, -0.7145311798163362926 ) ) ;
#2920=LINE ( 'NONE', #18777, #14976 ) ;
#2937=ADVANCED_FACE ( 'NONE', ( #3384 ), #12578, .T. ) ;
#3021=( LENGTH_UNIT ( ) NAMED_UNIT ( * ) SI_UNIT ( .MILLI., .METRE. ) );
#3069=ORIENTED_EDGE ( 'NONE', *, *, #23686, .T. ) ;
#3074=EDGE_CURVE ( 'NONE', #1424, #887, #5794, .T. ) ;
#3117=EDGE_CURVE ( 'NONE', #570, #12491, #17523, .T. ) ;
#3157=FACE_OUTER_BOUND ( 'NONE', #9557, .T. ) ;
#3244=CARTESIAN_POINT ( 'NONE',  ( 0.000000000000000000, 0.000000000000000000, 0.000000000000000000 ) ) ;
#3256=AXIS2_PLACEMENT_3D ( 'NONE', #29199, #19541, #942 ) ;
#3270=CARTESIAN_POINT ( 'NONE',  ( 8.000000000000001776, 4.336808689942017736E-15, -5.000000000000000888 ) ) ;
#3277=AXIS2_PLACEMENT_3D ( 'NONE', #22584, #29818, #6253 ) ;
#3330=DIRECTION ( 'NONE',  ( 0.000000000000000000, 0.000000000000000000, 1.000000000000000000 ) ) ;
#3384=FACE_OUTER_BOUND ( 'NONE', #16591, .T. ) ;
#3408=EDGE_CURVE ( 'NONE', #570, #887, #15361, .T. ) ;
#3421=CARTESIAN_POINT ( 'NONE',  ( -7.345652830558757174, 4.996589667937388235, -4.503584543331204060 ) ) ;
#3435=CARTESIAN_POINT ( 'NONE',  ( 0.000000000000000000, 0.000000000000000000, -5.000000000000000888 ) ) ;
#3467=DIRECTION ( 'NONE',  ( -0.000000000000000000, -0.000000000000000000, 1.000000000000000000 ) ) ;
#3525=ORIENTED_EDGE ( 'NONE', *, *, #22283, .T. ) ;
#3540=ORIENTED_EDGE ( 'NONE', *, *, #24659, .F. ) ;
#3547=ADVANCED_FACE ( 'NONE', ( #19149 ), #9741, .F. ) ;
#3566=EDGE_LOOP ( 'NONE', ( #23777, #5741, #3837 ) ) ;
#3619=CARTESIAN_POINT ( 'NONE',  ( 5.637851296924623057E-15, 9.237604307034036566, -4.285468820183664818 ) ) ;
#3622=PLANE ( 'NONE',  #29074 ) ;
#3623=ORIENTED_EDGE ( 'NONE', *, *, #21344, .F. ) ;
#3681=CARTESIAN_POINT ( 'NONE',  ( -4.250000000000003553, -1.366904252225140556E-15, -5.000000000000000888 ) ) ;
#3749=EDGE_CURVE ( 'NONE', #27863, #4596, #19685, .T. ) ;
#3755=PRODUCT_DEFINITION_SHAPE ( 'NONE', 'NONE',  #7839 ) ;
#3772=DIRECTION ( 'NONE',  ( 1.000000000000000000, 4.440892098500622217E-16, 0.000000000000000000 ) ) ;
#3825=EDGE_CURVE ( 'NONE', #29239, #6973, #6852, .T. ) ;
#3837=ORIENTED_EDGE ( 'NONE', *, *, #2310, .F. ) ;
#3858=DIRECTION ( 'NONE',  ( -0.000000000000000000, -0.000000000000000000, -1.000000000000000000 ) ) ;
#3877=AXIS2_PLACEMENT_3D ( 'NONE', #9701, #23304, #4679 ) ;
#3911=CARTESIAN_POINT ( 'NONE',  ( 7.345652830558766055, -4.996589667937400669, -0.4964154566688059877 ) ) ;
#3921=DIRECTION ( 'NONE',  ( -0.000000000000000000, -0.000000000000000000, 1.000000000000000000 ) ) ;
#3924=CARTESIAN_POINT ( 'NONE',  ( -4.683753385137379155E-14, -9.237604307034027684, -4.285468820183664818 ) ) ;
#3957=EDGE_CURVE ( 'NONE', #6726, #16400, #13435, .T. ) ;
#3968=FACE_OUTER_BOUND ( 'NONE', #10680, .T. ) ;
#4018=ADVANCED_FACE ( 'NONE', ( #17828 ), #16158, .F. ) ;
#4069=DIRECTION ( 'NONE',  ( -1.000000000000000000, -4.440892098500622217E-16, 0.000000000000000000 ) ) ;
#4103=ORIENTED_EDGE ( 'NONE', *, *, #20033, .F. ) ;
#4113=CARTESIAN_POINT ( 'NONE',  ( -8.000000000000000000, 4.618802153517001408, -5.000000000000000888 ) ) ;
#4122=CARTESIAN_POINT ( 'NONE',  ( -6.689127551062014732, -5.375634714784644608, -0.3173508448886681044 ) ) ;
#4197=ADVANCED_FACE ( 'NONE', ( #4698 ), #13680, .T. ) ;
#4385=DIRECTION ( 'NONE',  ( 1.000000000000000000, 4.440892098500622217E-16, 0.000000000000000000 ) ) ;
#4389=CIRCLE ( 'NONE', #7309, 8.000000000000005329 ) ;
#4402=ADVANCED_FACE ( 'NONE', ( #24236 ), #23941, .T. ) ;
#4453=CIRCLE ( 'NONE', #7372, 8.000000000000005329 ) ;
#4484=ORIENTED_EDGE ( 'NONE', *, *, #11831, .T. ) ;
#4566=CARTESIAN_POINT ( 'NONE',  ( 5.637851296924623057E-15, 9.237604307034036566, -0.7145311798163362926 ) ) ;
#4577=DIRECTION ( 'NONE',  ( -0.000000000000000000, -0.000000000000000000, -1.000000000000000000 ) ) ;
#4596=VERTEX_POINT ( 'NONE', #1528 ) ;
#4617=CARTESIAN_POINT ( 'NONE',  ( 8.000000000000012434, 3.115336682267024315, -0.3193931313915156500 ) ) ;
#4679=DIRECTION ( 'NONE',  ( 1.000000000000000000, 4.440892098500622217E-16, 0.000000000000000000 ) ) ;
#4689=PLANE ( 'NONE',  #25519 ) ;
#4698=FACE_OUTER_BOUND ( 'NONE', #18606, .T. ) ;
#4702=ORIENTED_EDGE ( 'NONE', *, *, #29927, .T. ) ;
#4710=CARTESIAN_POINT ( 'NONE',  ( -2.309976723937613219, 7.903938623646876493, -0.1306530452038166257 ) ) ;
#4741=EDGE_CURVE ( 'NONE', #15488, #1679, #4453, .T. ) ;
#4767=CARTESIAN_POINT ( 'NONE',  ( -8.000000000000000000, 4.618802153517001408, -5.000000000000000888 ) ) ;
#4797=FACE_OUTER_BOUND ( 'NONE', #20873, .T. ) ;
#4817=CYLINDRICAL_SURFACE ( 'NONE', #7375, 4.250000000000003553 ) ;
#4830=CARTESIAN_POINT ( 'NONE',  ( -7.999999999999994671, 3.115336682267016766, -4.680606868608490956 ) ) ;
#4902=AXIS2_PLACEMENT_3D ( 'NONE', #24536, #8346, #27006 ) ;
#4915=UNCERTAINTY_MEASURE_WITH_UNIT (LENGTH_MEASURE( 1.000000000000000082E-05 ), #25066, 'distance_accuracy_value', 'NONE');
#4921=ORIENTED_EDGE ( 'NONE', *, *, #12725, .T. ) ;
#5034=ORIENTED_EDGE ( 'NONE', *, *, #4741, .T. ) ;
#5154=EDGE_CURVE ( 'NONE', #5542, #19491, #24430, .T. ) ;
#5193=CARTESIAN_POINT ( 'NONE',  ( 6.689127551062008514, 5.375634714784629509, -4.682649155111342942 ) ) ;
#5264=ORIENTED_EDGE ( 'NONE', *, *, #18755, .F. ) ;
#5407=CARTESIAN_POINT ( 'NONE',  ( 5.637851296924623057E-15, 9.237604307034036566, -0.7145311798163362926 ) ) ;
#5435=CARTESIAN_POINT ( 'NONE',  ( 0.000000000000000000, 0.000000000000000000, 0.000000000000000000 ) ) ;
#5495=EDGE_LOOP ( 'NONE', ( #17701, #11171, #16511 ) ) ;
#5529=ORIENTED_EDGE ( 'NONE', *, *, #29253, .F. ) ;
#5542=VERTEX_POINT ( 'NONE', #14556 ) ;
#5572=CARTESIAN_POINT ( 'NONE',  ( -4.680456609903995258, -6.535341423375610859, -4.983111142572218100 ) ) ;
#5576=ORIENTED_EDGE ( 'NONE', *, *, #10661, .T. ) ;
#5595=LINE ( 'NONE', #28985, #15984 ) ;
#5606=CARTESIAN_POINT ( 'NONE',  ( 3.318518101603024295, 7.321656987762882984, -4.999999999999998224 ) ) ;
#5661=ORIENTED_EDGE ( 'NONE', *, *, #8903, .T. ) ;
#5669=DIRECTION ( 'NONE',  ( 1.000000000000000000, 4.440892098500622217E-16, 0.000000000000000000 ) ) ;
#5684=EDGE_LOOP ( 'NONE', ( #15353, #5529, #7970 ) ) ;
#5722=DIRECTION ( 'NONE',  ( 0.000000000000000000, 0.000000000000000000, 1.000000000000000000 ) ) ;
#5741=ORIENTED_EDGE ( 'NONE', *, *, #7539, .F. ) ;
#5748=FILL_AREA_STYLE_COLOUR ( '', #26845 ) ;
#5794=CIRCLE ( 'NONE', #22374, 8.000000000000005329 ) ;
#5828=EDGE_LOOP ( 'NONE', ( #6316, #14751, #15447 ) ) ;
#5832=CARTESIAN_POINT ( 'NONE',  ( -15.99999999999998224, -1.561251128379126385E-14, -5.000000000000000888 ) ) ;
#5853=COLOUR_RGB ( '', 0.31764706, 0.68627451, 0.89019608) ;
#5917=AXIS2_PLACEMENT_3D ( 'NONE', #12284, #17462, #17313 ) ;
#5979=VECTOR ( 'NONE', #2300, 1000.000000000000000 ) ;
#5994=CARTESIAN_POINT ( 'NONE',  ( 8.000000000000000000, -4.618802153517027165, -4.285468820183664818 ) ) ;
#6017=ORIENTED_EDGE ( 'NONE', *, *, #10245, .T. ) ;
#6041=CARTESIAN_POINT ( 'NONE',  ( -0.6543471694412855699, -8.859816792613662173, -0.4964154566688078751 ) ) ;
#6055=CARTESIAN_POINT ( 'NONE',  ( 2.645508037661892686, 7.710219529346620249, -4.931901280394563436 ) ) ;
#6124=CIRCLE ( 'NONE', #13433, 4.250000000000003553 ) ;
#6178=CIRCLE ( 'NONE', #20295, 8.000000000000005329 ) ;
#6204=DIRECTION ( 'NONE',  ( 0.8660254037844375974, -0.5000000000000016653, 0.000000000000000000 ) ) ;
#6210=CARTESIAN_POINT ( 'NONE',  ( 3.319543390096043378, -7.321065037175453760, -4.983111142572217211 ) ) ;
#6211=ORIENTED_EDGE ( 'NONE', *, *, #27803, .T. ) ;
#6214=ORIENTED_EDGE ( 'NONE', *, *, #23686, .F. ) ;
#6253=DIRECTION ( 'NONE',  ( 1.000000000000000000, 4.440892098500622217E-16, 0.000000000000000000 ) ) ;
#6266=ADVANCED_FACE ( 'NONE', ( #20304, #20155 ), #8555, .F. ) ;
#6293=CARTESIAN_POINT ( 'NONE',  ( 8.000000000000014211, -3.098204225878181006, -4.684209322808117193 ) ) ;
#6316=ORIENTED_EDGE ( 'NONE', *, *, #22458, .T. ) ;
#6358=CIRCLE ( 'NONE', #14130, 4.250000000000003553 ) ;
#6409=FACE_OUTER_BOUND ( 'NONE', #27575, .T. ) ;
#6438=DIRECTION ( 'NONE',  ( 0.000000000000000000, -0.000000000000000000, 1.000000000000000000 ) ) ;
#6509=CARTESIAN_POINT ( 'NONE',  ( -1.313474075707254052, -8.479269695850879529, -4.683279549040147316 ) ) ;
#6586=CARTESIAN_POINT ( 'NONE',  ( 0.000000000000000000, 0.000000000000000000, -5.000000000000000888 ) ) ;
#6595=SURFACE_STYLE_FILL_AREA ( #2037 ) ;
#6607=CARTESIAN_POINT ( 'NONE',  ( 8.000000000000014211, 1.572549600175628060, -0.06894455525514016359 ) ) ;
#6624=VERTEX_POINT ( 'NONE', #28999 ) ;
#6670=ORIENTED_EDGE ( 'NONE', *, *, #26054, .F. ) ;
#6706=ORIENTED_EDGE ( 'NONE', *, *, #3749, .T. ) ;
#6718=VERTEX_POINT ( 'NONE', #11086 ) ;
#6726=VERTEX_POINT ( 'NONE', #13674 ) ;
#6732=ORIENTED_EDGE ( 'NONE', *, *, #11958, .F. ) ;
#6745=EDGE_LOOP ( 'NONE', ( #7962, #14115 ) ) ;
#6750=PRODUCT_CONTEXT ( 'NONE', #27655, 'mechanical' ) ;
#6836=VECTOR ( 'NONE', #3330, 1000.000000000000000 ) ;
#6852=CIRCLE ( 'NONE', #515, 8.000000000000005329 ) ;
#6951=ADVANCED_FACE ( 'NONE', ( #18554 ), #4817, .F. ) ;
#6967=B_SPLINE_CURVE_WITH_KNOTS ( 'NONE', 3,
 ( #12893, #6041, #8470, #1320, #13205, #10609 ),
 .UNSPECIFIED., .F., .F.,
 ( 4, 2, 4 ),
 ( 2.380731630115174505E-07, 0.002336973833157602806, 0.004673709593152193878 ),
 .UNSPECIFIED. ) ;
#6973=VERTEX_POINT ( 'NONE', #23139 ) ;
#7001=CARTESIAN_POINT ( 'NONE',  ( 0.000000000000000000, 0.000000000000000000, -5.000000000000000888 ) ) ;
#7118=ADVANCED_FACE ( 'NONE', ( #3157 ), #26399, .T. ) ;
#7127=CARTESIAN_POINT ( 'NONE',  ( -8.000000000000000000, 4.618802153517028941, -4.285468820183664818 ) ) ;
#7191=CARTESIAN_POINT ( 'NONE',  ( 4.339467034331203621, 6.732211846623402884, -3.988960492936253045E-15 ) ) ;
#7249=CARTESIAN_POINT ( 'NONE',  ( 8.000000000000010658, 4.618802153517005848, -5.000000000000000888 ) ) ;
#7309=AXIS2_PLACEMENT_3D ( 'NONE', #16750, #1337, #3772 ) ;
#7336=ORIENTED_EDGE ( 'NONE', *, *, #21344, .T. ) ;
#7372=AXIS2_PLACEMENT_3D ( 'NONE', #27783, #16592, #25917 ) ;
#7375=AXIS2_PLACEMENT_3D ( 'NONE', #401, #9686, #16570 ) ;
#7403=DIRECTION ( 'NONE',  ( 0.000000000000000000, 0.000000000000000000, 1.000000000000000000 ) ) ;
#7435=B_SPLINE_CURVE_WITH_KNOTS ( 'NONE', 3,
 ( #1438, #15454, #22490, #10270, #17295, #24476 ),
 .UNSPECIFIED., .F., .F.,
 ( 4, 2, 4 ),
 ( 0.008240550023493518894, 0.01057684187039405199, 0.01291313371729458509 ),
 .UNSPECIFIED. ) ;
#7506=CARTESIAN_POINT ( 'NONE',  ( -5.000000000000006217, -2.220446049250313870E-15, -4.974599999999998801 ) ) ;
#7508=AXIS2_PLACEMENT_3D ( 'NONE', #24711, #12940, #22413 ) ;
#7511=CARTESIAN_POINT ( 'NONE',  ( 5.637851296924623057E-15, 9.237604307034036566, -0.7145311798163362926 ) ) ;
#7539=EDGE_CURVE ( 'NONE', #16400, #1424, #6967, .T. ) ;
#7545=CARTESIAN_POINT ( 'NONE',  ( -4.683753385137379155E-14, -9.237604307034027684, -0.7145311798163362926 ) ) ;
#7655=CARTESIAN_POINT ( 'NONE',  ( 0.000000000000000000, 0.000000000000000000, -5.000000000000000888 ) ) ;
#7690=CARTESIAN_POINT ( 'NONE',  ( 4.000000000000008882, -6.928203230275510549, 0.000000000000000000 ) ) ;
#7711=CARTESIAN_POINT ( 'NONE',  ( 5.000000000000005329, 2.220446049250313475E-15, 0.000000000000000000 ) ) ;
#7813=CARTESIAN_POINT ( 'NONE',  ( 4.681481898397010788, -6.534749472788171865, -4.999999999999988454 ) ) ;
#7818=LINE ( 'NONE', #17126, #15941 ) ;
#7839=PRODUCT_DEFINITION ( 'UNKNOWN', '', #19498, #20779 ) ;
#7850=DIRECTION ( 'NONE',  ( -1.000000000000000000, -4.440892098500622217E-16, 0.000000000000000000 ) ) ;
#7896=ORIENTED_EDGE ( 'NONE', *, *, #8903, .F. ) ;
#7962=ORIENTED_EDGE ( 'NONE', *, *, #14270, .F. ) ;
#7970=ORIENTED_EDGE ( 'NONE', *, *, #10245, .F. ) ;
#7994=DIRECTION ( 'NONE',  ( 1.000000000000000000, 4.440892098500622217E-16, 0.000000000000000000 ) ) ;
#8022=FACE_OUTER_BOUND ( 'NONE', #761, .T. ) ;
#8136=CARTESIAN_POINT ( 'NONE',  ( -4.000000000000020428, -6.928203230275511437, -5.000000000000000888 ) ) ;
#8162=DIRECTION ( 'NONE',  ( 1.000000000000000000, 4.440892098500622217E-16, 0.000000000000000000 ) ) ;
#8203=VERTEX_POINT ( 'NONE', #11320 ) ;
#8336=CARTESIAN_POINT ( 'NONE',  ( 0.000000000000000000, 0.000000000000000000, -4.449444346342715129 ) ) ;
#8346=DIRECTION ( 'NONE',  ( 0.000000000000000000, 0.000000000000000000, 1.000000000000000000 ) ) ;
#8354=CARTESIAN_POINT ( 'NONE',  ( 8.000000000000000000, -4.618802153517027165, -0.7145311798163362926 ) ) ;
#8361=AXIS2_PLACEMENT_3D ( 'NONE', #3435, #12727, #10285 ) ;
#8391=FACE_OUTER_BOUND ( 'NONE', #24400, .T. ) ;
#8404=CARTESIAN_POINT ( 'NONE',  ( -7.372574772901430151E-15, -9.237604307034054330, -5.000000000000000888 ) ) ;
#8470=CARTESIAN_POINT ( 'NONE',  ( -1.313474075707253608, -8.479269695850879529, -0.3167204509598532947 ) ) ;
#8473=DIRECTION ( 'NONE',  ( -0.8660254037844375974, 0.5000000000000017764, -0.000000000000000000 ) ) ;
#8486=CARTESIAN_POINT ( 'NONE',  ( 3.660532965668829686, -7.124194613927646635, -4.999999999999990230 ) ) ;
#8546=ORIENTED_EDGE ( 'NONE', *, *, #20208, .T. ) ;
#8555=PLANE ( 'NONE',  #53 ) ;
#8624=CARTESIAN_POINT ( 'NONE',  ( 4.681481898397010788, -6.534749472788171865, -1.177036983504575751E-14 ) ) ;
#8679=AXIS2_PLACEMENT_3D ( 'NONE', #7655, #16961, #26287 ) ;
#8688=B_SPLINE_CURVE_WITH_KNOTS ( 'NONE', 3,
 ( #7511, #11467, #202, #23238, #14360, #51 ),
 .UNSPECIFIED., .F., .F.,
 ( 4, 2, 4 ),
 ( 2.380731629581706008E-07, 0.002336973833157567244, 0.004673709593152178265 ),
 .UNSPECIFIED. ) ;
#8732=ORIENTED_EDGE ( 'NONE', *, *, #14874, .T. ) ;
#8775=PLANE ( 'NONE',  #19759 ) ;
#8817=DIRECTION ( 'NONE',  ( 0.8660254037844378194, 0.5000000000000014433, 0.000000000000000000 ) ) ;
#8845=CARTESIAN_POINT ( 'NONE',  ( -8.000000000000001776, -4.336808689942017736E-15, 0.000000000000000000 ) ) ;
#8903=EDGE_CURVE ( 'NONE', #2266, #570, #13864, .T. ) ;
#8964=CYLINDRICAL_SURFACE ( 'NONE', #10010, 4.250000000000003553 ) ;
#9076=ORIENTED_EDGE ( 'NONE', *, *, #21639, .T. ) ;
#9090=CARTESIAN_POINT ( 'NONE',  ( -1.310872448937994594, 8.480771745766412906, -4.682649155111336725 ) ) ;
#9098=CONICAL_SURFACE ( 'NONE', #3277, 8.000000000000007105, 1.047197551196596077 ) ;
#9121=DIRECTION ( 'NONE',  ( 1.000000000000000000, 4.440892098500622217E-16, 0.000000000000000000 ) ) ;
#9143=ORIENTED_EDGE ( 'NONE', *, *, #20208, .F. ) ;
#9151=CARTESIAN_POINT ( 'NONE',  ( 7.347286611336969031, 4.995646404165290377, -0.4969600502617546600 ) ) ;
#9274=CARTESIAN_POINT ( 'NONE',  ( 6.505213034913026604E-15, 9.237604307034033013, -5.000000000000000888 ) ) ;
#9310=CARTESIAN_POINT ( 'NONE',  ( 5.690023276062400548, 5.952467836904161480, -4.869346954796185400 ) ) ;
#9334=ORIENTED_EDGE ( 'NONE', *, *, #24659, .T. ) ;
#9353=CARTESIAN_POINT ( 'NONE',  ( -8.000000000000000000, 4.618802153517028941, -4.285468820183664818 ) ) ;
#9360=FACE_OUTER_BOUND ( 'NONE', #2862, .T. ) ;
#9456=CARTESIAN_POINT ( 'NONE',  ( 4.680456609903983711, 6.535341423375600201, -0.01688885742777455554 ) ) ;
#9482=LINE ( 'NONE', #4767, #16888 ) ;
#9509=PLANE ( 'NONE',  #28116 ) ;
#9521=DIRECTION ( 'NONE',  ( 1.000000000000000000, 4.440892098500622217E-16, 0.000000000000000000 ) ) ;
#9557=EDGE_LOOP ( 'NONE', ( #15232, #29224, #11408 ) ) ;
#9558=AXIS2_PLACEMENT_3D ( 'NONE', #10831, #17695, #2003 ) ;
#9653=AXIS2_PLACEMENT_3D ( 'NONE', #2892, #26085, #9121 ) ;
#9686=DIRECTION ( 'NONE',  ( 0.000000000000000000, 0.000000000000000000, 1.000000000000000000 ) ) ;
#9701=CARTESIAN_POINT ( 'NONE',  ( 0.000000000000000000, 0.000000000000000000, 0.000000000000000000 ) ) ;
#9741=CONICAL_SURFACE ( 'NONE', #28387, 4.175000000000003375, 0.9599310885968852514 ) ;
#9763=ORIENTED_EDGE ( 'NONE', *, *, #29324, .T. ) ;
#9784=DIRECTION ( 'NONE',  ( -0.8191520442889924647, -3.637765840953617664E-16, -0.5735764363510452712 ) ) ;
#9806=ORIENTED_EDGE ( 'NONE', *, *, #29253, .T. ) ;
#9823=CARTESIAN_POINT ( 'NONE',  ( 0.6527133886630125392, -8.860760056385789341, -0.4969600502617795290 ) ) ;
#9832=DIRECTION ( 'NONE',  ( 0.000000000000000000, 0.000000000000000000, -1.000000000000000000 ) ) ;
#9935=CARTESIAN_POINT ( 'NONE',  ( -7.345652830558765167, 4.996589667937382018, -0.4964154566688006032 ) ) ;
#9947=ORIENTED_EDGE ( 'NONE', *, *, #2314, .T. ) ;
#10003=( NAMED_UNIT ( * ) PLANE_ANGLE_UNIT ( ) SI_UNIT ( $, .RADIAN. ) );
#10004=ORIENTED_EDGE ( 'NONE', *, *, #29573, .T. ) ;
#10010=AXIS2_PLACEMENT_3D ( 'NONE', #11858, #23319, #21172 ) ;
#10039=AXIS2_PLACEMENT_3D ( 'NONE', #26640, #9832, #7850 ) ;
#10040=CARTESIAN_POINT ( 'NONE',  ( 0.000000000000000000, 0.000000000000000000, -0.5251556536572770106 ) ) ;
#10064=CONICAL_SURFACE ( 'NONE', #1331, 4.175000000000003375, 0.9599310885968852514 ) ;
#10073=ORIENTED_EDGE ( 'NONE', *, *, #2310, .T. ) ;
#10156=SURFACE_STYLE_USAGE ( .BOTH. , #869 ) ;
#10194=DIRECTION ( 'NONE',  ( 1.000000000000000000, 4.440892098500622217E-16, 0.000000000000000000 ) ) ;
#10237=CARTESIAN_POINT ( 'NONE',  ( -4.681481898397005459, 6.534749472788154101, -2.430984558619841973E-15 ) ) ;
#10238=CARTESIAN_POINT ( 'NONE',  ( 8.000000000000000000, -4.618802153517027165, -4.285468820183664818 ) ) ;
#10245=EDGE_CURVE ( 'NONE', #8203, #19707, #1453, .T. ) ;
#10270=CARTESIAN_POINT ( 'NONE',  ( -7.999999999999994671, -1.555946510856153431, -4.932911297836646725 ) ) ;
#10285=DIRECTION ( 'NONE',  ( 1.000000000000000000, 4.440892098500622217E-16, 0.000000000000000000 ) ) ;
#10311=ADVANCED_FACE ( 'NONE', ( #11263 ), #4689, .T. ) ;
#10317=CARTESIAN_POINT ( 'NONE',  ( 1.313474075707222966, 8.479269695850875976, -4.683279549040151757 ) ) ;
#10324=DIRECTION ( 'NONE',  ( 1.000000000000000000, 4.440892098500622217E-16, 0.000000000000000000 ) ) ;
#10363=ORIENTED_EDGE ( 'NONE', *, *, #14912, .F. ) ;
#10408=CARTESIAN_POINT ( 'NONE',  ( 8.000000000000014211, -0.7805016046290974563, -4.999999999999993783 ) ) ;
#10436=DIRECTION ( 'NONE',  ( 0.000000000000000000, 0.000000000000000000, 1.000000000000000000 ) ) ;
#10446=DIRECTION ( 'NONE',  ( 1.000000000000000000, 0.000000000000000000, 0.000000000000000000 ) ) ;
#10451=B_SPLINE_CURVE_WITH_KNOTS ( 'NONE', 3,
 ( #28133, #7191, #9456, #16333, #21367, #13885, #9151, #14332 ),
 .UNSPECIFIED., .F., .F.,
 ( 4, 2, 2, 4 ),
 ( 0.004673709593152178265, 0.005837709341827659881, 0.007001709090503141497, 0.009329708587854104729 ),
 .UNSPECIFIED. ) ;
#10527=CIRCLE ( 'NONE', #3256, 8.000000000000007105 ) ;
#10587=AXIS2_PLACEMENT_3D ( 'NONE', #29538, #20607, #13597 ) ;
#10600=ORIENTED_EDGE ( 'NONE', *, *, #11831, .F. ) ;
#10607=B_SPLINE_CURVE_WITH_KNOTS ( 'NONE', 3,
 ( #20380, #8486, #6210, #27147, #18094, #15502, #24833, #3924 ),
 .UNSPECIFIED., .F., .F.,
 ( 4, 2, 2, 4 ),
 ( 0.004673709593152139234, 0.005837709341827639065, 0.007001709090503138895, 0.009329708587854137689 ),
 .UNSPECIFIED. ) ;
#10608=ORIENTED_EDGE ( 'NONE', *, *, #14689, .T. ) ;
#10609=CARTESIAN_POINT ( 'NONE',  ( -4.000000000000020428, -6.928203230275511437, 0.000000000000000000 ) ) ;
#10659=EDGE_CURVE ( 'NONE', #15781, #1679, #12670, .T. ) ;
#10661=EDGE_CURVE ( 'NONE', #19491, #5542, #6124, .T. ) ;
#10680=EDGE_LOOP ( 'NONE', ( #6706, #6211, #3623 ) ) ;
#10701=ORIENTED_EDGE ( 'NONE', *, *, #3749, .F. ) ;
#10716=FILL_AREA_STYLE_COLOUR ( '', #5853 ) ;
#10761=AXIS2_PLACEMENT_3D ( 'NONE', #7001, #2881, #23320 ) ;
#10777=FACE_OUTER_BOUND ( 'NONE', #15549, .T. ) ;
#10825=EDGE_LOOP ( 'NONE', ( #4702, #4921, #23581, #6214 ) ) ;
#10831=CARTESIAN_POINT ( 'NONE',  ( 0.000000000000000000, 0.000000000000000000, 0.000000000000000000 ) ) ;
#10844=DIRECTION ( 'NONE',  ( 1.000000000000000000, 4.440892098500622217E-16, 0.000000000000000000 ) ) ;
#10857=EDGE_LOOP ( 'NONE', ( #17434, #28235, #12748, #7336, #19800, #5034 ) ) ;
#10860=SURFACE_STYLE_USAGE ( .BOTH. , #27542 ) ;
#10897=CARTESIAN_POINT ( 'NONE',  ( 0.000000000000000000, 0.000000000000000000, 0.000000000000000000 ) ) ;
#10940=CARTESIAN_POINT ( 'NONE',  ( -3.660532965668825689, 7.124194613927628872, -4.999999999999999112 ) ) ;
#10974=CARTESIAN_POINT ( 'NONE',  ( -5.355005115540915739, -6.145890662064674714, -0.08224679563972937812 ) ) ;
#10998=DIRECTION ( 'NONE',  ( -0.000000000000000000, -0.000000000000000000, -1.000000000000000000 ) ) ;
#11086=CARTESIAN_POINT ( 'NONE',  ( -4.250000000000000000, -1.366904252225139372E-15, -0.5251556536572770106 ) ) ;
#11095=CYLINDRICAL_SURFACE ( 'NONE', #25978, 5.000000000000006217 ) ;
#11157=CARTESIAN_POINT ( 'NONE',  ( 4.339467034331203621, 6.732211846623402884, -4.999999999999996447 ) ) ;
#11171=ORIENTED_EDGE ( 'NONE', *, *, #10659, .T. ) ;
#11263=FACE_OUTER_BOUND ( 'NONE', #20716, .T. ) ;
#11283=ADVANCED_FACE ( 'NONE', ( #29265 ), #21498, .T. ) ;
#11320=CARTESIAN_POINT ( 'NONE',  ( -8.000000000000000000, 4.618802153517001408, -0.7145311798163294092 ) ) ;
#11346=CARTESIAN_POINT ( 'NONE',  ( 8.000000000000008882, 3.115336682267025203, -4.680606868608483850 ) ) ;
#11387=CARTESIAN_POINT ( 'NONE',  ( -3.319543390096040270, 7.321065037175434220, -4.983111142572229646 ) ) ;
#11408=ORIENTED_EDGE ( 'NONE', *, *, #3408, .F. ) ;
#11424=DIRECTION ( 'NONE',  ( 0.000000000000000000, 0.000000000000000000, -1.000000000000000000 ) ) ;
#11467=CARTESIAN_POINT ( 'NONE',  ( 0.6543471694412490436, 8.859816792613667502, -0.4964154566688076531 ) ) ;
#11535=CARTESIAN_POINT ( 'NONE',  ( 4.000000000000019540, 6.928203230275512325, -5.000000000000000888 ) ) ;
#11552=AXIS2_PLACEMENT_3D ( 'NONE', #6586, #10998, #30142 ) ;
#11597=CARTESIAN_POINT ( 'NONE',  ( 0.000000000000000000, 0.000000000000000000, -0.5776712190230064436 ) ) ;
#11610=AXIS2_PLACEMENT_3D ( 'NONE', #9274, #16456, #23330 ) ;
#11616=EDGE_CURVE ( 'NONE', #24955, #19224, #19254, .T. ) ;
#11638=ORIENTED_EDGE ( 'NONE', *, *, #7539, .T. ) ;
#11648=ORIENTED_EDGE ( 'NONE', *, *, #5154, .T. ) ;
#11725=FACE_OUTER_BOUND ( 'NONE', #3566, .T. ) ;
#11831=EDGE_CURVE ( 'NONE', #26232, #13323, #7818, .T. ) ;
#11842=CARTESIAN_POINT ( 'NONE',  ( -8.000000000000001776, -4.336808689942017736E-15, -5.000000000000000888 ) ) ;
#11858=CARTESIAN_POINT ( 'NONE',  ( 0.000000000000000000, 0.000000000000000000, -5.000000000000000888 ) ) ;
#11882=ORIENTED_EDGE ( 'NONE', *, *, #11616, .T. ) ;
#11899=EDGE_CURVE ( 'NONE', #28625, #1424, #23761, .T. ) ;
#11919=UNCERTAINTY_MEASURE_WITH_UNIT (LENGTH_MEASURE( 1.000000000000000082E-05 ), #25221, 'distance_accuracy_value', 'NONE');
#11958=EDGE_CURVE ( 'NONE', #24955, #6624, #2832, .T. ) ;
#11964=CARTESIAN_POINT ( 'NONE',  ( 0.000000000000000000, 0.000000000000000000, -0.5776712190230064436 ) ) ;
#11986=AXIS2_PLACEMENT_3D ( 'NONE', #25870, #14242, #14389 ) ;
#12037=CARTESIAN_POINT ( 'NONE',  ( 8.000000000000001776, 4.336808689942017736E-15, 0.000000000000000000 ) ) ;
#12054=CARTESIAN_POINT ( 'NONE',  ( 8.000000000000003553, 4.618802153517037823, -4.285468820183664818 ) ) ;
#12074=EDGE_CURVE ( 'NONE', #19491, #19224, #2920, .T. ) ;
#12081=DIRECTION ( 'NONE',  ( 0.000000000000000000, 0.000000000000000000, 1.000000000000000000 ) ) ;
#12284=CARTESIAN_POINT ( 'NONE',  ( 0.000000000000000000, 0.000000000000000000, 0.000000000000000000 ) ) ;
#12327=DIRECTION ( 'NONE',  ( -0.000000000000000000, -0.000000000000000000, -1.000000000000000000 ) ) ;
#12376=ADVANCED_BREP_SHAPE_REPRESENTATION ( '', ( #1835, #13190 ), #496 ) ;
#12429=CARTESIAN_POINT ( 'NONE',  ( 4.250000000000003553, 1.887379141862766119E-15, -0.5251556536572770106 ) ) ;
#12481=CIRCLE ( 'NONE', #29627, 8.000000000000007105 ) ;
#12491=VERTEX_POINT ( 'NONE', #19978 ) ;
#12513=ADVANCED_FACE ( 'NONE', ( #6409 ), #15698, .T. ) ;
#12521=DIRECTION ( 'NONE',  ( 0.000000000000000000, 0.000000000000000000, 1.000000000000000000 ) ) ;
#12571=CARTESIAN_POINT ( 'NONE',  ( -8.000000000000003553, -4.618802153517037823, -4.285468820183664818 ) ) ;
#12578=CONICAL_SURFACE ( 'NONE', #8679, 8.000000000000007105, 1.047197551196596077 ) ;
#12600=( NAMED_UNIT ( * ) SI_UNIT ( $, .STERADIAN. ) SOLID_ANGLE_UNIT ( ) );
#12621=ORIENTED_EDGE ( 'NONE', *, *, #29485, .T. ) ;
#12636=EDGE_LOOP ( 'NONE', ( #28657, #25704, #11882, #18494 ) ) ;
#12637=DIRECTION ( 'NONE',  ( 1.000000000000000000, 4.440892098500622217E-16, 0.000000000000000000 ) ) ;
#12670=B_SPLINE_CURVE_WITH_KNOTS ( 'NONE', 3,
 ( #3619, #14883, #10317, #6055, #5606, #1184 ),
 .UNSPECIFIED., .F., .F.,
 ( 4, 2, 4 ),
 ( 2.380731629581860062E-07, 0.002336973833157567678, 0.004673709593152178265 ),
 .UNSPECIFIED. ) ;
#12725=EDGE_CURVE ( 'NONE', #6718, #26068, #5595, .T. ) ;
#12727=DIRECTION ( 'NONE',  ( 0.000000000000000000, 0.000000000000000000, 1.000000000000000000 ) ) ;
#12748=ORIENTED_EDGE ( 'NONE', *, *, #14912, .T. ) ;
#12847=ORIENTED_EDGE ( 'NONE', *, *, #17279, .F. ) ;
#12871=FACE_OUTER_BOUND ( 'NONE', #26568, .T. ) ;
#12893=CARTESIAN_POINT ( 'NONE',  ( -4.683753385137379155E-14, -9.237604307034027684, -0.7145311798163362926 ) ) ;
#12894=B_SPLINE_CURVE_WITH_KNOTS ( 'NONE', 3,
 ( #27552, #13614, #6607, #4617, #22944, #18345 ),
 .UNSPECIFIED., .F., .F.,
 ( 4, 2, 4 ),
 ( 0.01291313371729459203, 0.01525081363757311605, 0.01758849355785164006 ),
 .UNSPECIFIED. ) ;
#12910=CARTESIAN_POINT ( 'NONE',  ( 0.000000000000000000, 0.000000000000000000, -4.449444346342715129 ) ) ;
#12921=ORIENTED_EDGE ( 'NONE', *, *, #22283, .F. ) ;
#12940=DIRECTION ( 'NONE',  ( 0.000000000000000000, 0.000000000000000000, 1.000000000000000000 ) ) ;
#13045=DIRECTION ( 'NONE',  ( 0.000000000000000000, 0.000000000000000000, 1.000000000000000000 ) ) ;
#13104=ADVANCED_FACE ( 'NONE', ( #28761 ), #17111, .F. ) ;
#13109=CARTESIAN_POINT ( 'NONE',  ( -8.000000000000003553, -4.618802153517037823, -0.7145311798163362926 ) ) ;
#13160=STYLED_ITEM ( 'NONE', ( #13451 ), #12376 ) ;
#13186=ORIENTED_EDGE ( 'NONE', *, *, #18612, .T. ) ;
#13190=AXIS2_PLACEMENT_3D ( 'NONE', #5435, #19606, #10446 ) ;
#13205=CARTESIAN_POINT ( 'NONE',  ( -3.318518101603040726, -7.321656987762888313, -1.321710210895610091E-14 ) ) ;
#13242=CARTESIAN_POINT ( 'NONE',  ( 0.000000000000000000, 0.000000000000000000, -25.03750572909317285 ) ) ;
#13304=PLANE ( 'NONE',  #11610 ) ;
#13308=ORIENTED_EDGE ( 'NONE', *, *, #3957, .T. ) ;
#13323=VERTEX_POINT ( 'NONE', #16784 ) ;
#13353=FACE_OUTER_BOUND ( 'NONE', #14445, .T. ) ;
#13366=CARTESIAN_POINT ( 'NONE',  ( -2.645508037661914891, -7.710219529346629130, -4.931901280394557219 ) ) ;
#13391=CARTESIAN_POINT ( 'NONE',  ( -7.999999999999998224, 3.115336682266997670, -0.3193931313915031045 ) ) ;
#13407=DIRECTION ( 'NONE',  ( -1.000000000000000000, -4.440892098500622217E-16, 0.000000000000000000 ) ) ;
#13409=CARTESIAN_POINT ( 'NONE',  ( -7.999999999999994671, -1.555946510856154985, -0.06708870216335502401 ) ) ;
#13433=AXIS2_PLACEMENT_3D ( 'NONE', #12910, #3467, #15193 ) ;
#13435=LINE ( 'NONE', #8404, #21528 ) ;
#13451=PRESENTATION_STYLE_ASSIGNMENT (( #10860 ) ) ;
#13485=CARTESIAN_POINT ( 'NONE',  ( 8.000000000000014211, 1.572549600175630502, -4.931055444744863792 ) ) ;
#13540=ORIENTED_EDGE ( 'NONE', *, *, #25576, .F. ) ;
#13548=AXIS2_PLACEMENT_3D ( 'NONE', #347, #26439, #5669 ) ;
#13594=DIRECTION ( 'NONE',  ( -0.000000000000000000, -0.000000000000000000, -1.000000000000000000 ) ) ;
#13597=DIRECTION ( 'NONE',  ( 1.000000000000000000, 4.440892098500622217E-16, 0.000000000000000000 ) ) ;
#13614=CARTESIAN_POINT ( 'NONE',  ( 8.000000000000010658, 0.7809653281576138806, -7.280248181650708259E-15 ) ) ;
#13668=CARTESIAN_POINT ( 'NONE',  ( -4.000000000000020428, -6.928203230275511437, -5.000000000000000888 ) ) ;
#13674=CARTESIAN_POINT ( 'NONE',  ( -4.683753385137379155E-14, -9.237604307034027684, -4.285468820183664818 ) ) ;
#13680=CONICAL_SURFACE ( 'NONE', #10761, 8.000000000000007105, 1.047197551196596077 ) ;
#13690=ORIENTED_EDGE ( 'NONE', *, *, #24948, .F. ) ;
#13793=DIRECTION ( 'NONE',  ( -1.000000000000000000, -4.440892098500622217E-16, 0.000000000000000000 ) ) ;
#13859=ADVANCED_FACE ( 'NONE', ( #16444 ), #8964, .F. ) ;
#13860=CARTESIAN_POINT ( 'NONE',  ( -4.680456609903995258, -6.535341423375610859, -0.01688885742778332977 ) ) ;
#13864=LINE ( 'NONE', #16769, #5979 ) ;
#13871=ORIENTED_EDGE ( 'NONE', *, *, #30232, .T. ) ;
#13885=CARTESIAN_POINT ( 'NONE',  ( 6.689127551062008514, 5.375634714784629509, -0.3173508448886592226 ) ) ;
#14026=AXIS2_PLACEMENT_3D ( 'NONE', #3244, #945, #23849 ) ;
#14115=ORIENTED_EDGE ( 'NONE', *, *, #26991, .F. ) ;
#14118=STYLED_ITEM ( 'NONE', ( #15033 ), #1835 ) ;
#14130=AXIS2_PLACEMENT_3D ( 'NONE', #304, #4577, #18756 ) ;
#14242=DIRECTION ( 'NONE',  ( 0.000000000000000000, 0.000000000000000000, -1.000000000000000000 ) ) ;
#14270=EDGE_CURVE ( 'NONE', #23525, #26068, #1308, .T. ) ;
#14275=ORIENTED_EDGE ( 'NONE', *, *, #22417, .T. ) ;
#14298=B_SPLINE_CURVE_WITH_KNOTS ( 'NONE', 3,
 ( #14840, #3421, #17294, #28948, #24177, #1138 ),
 .UNSPECIFIED., .F., .F.,
 ( 4, 2, 4 ),
 ( 2.380731629704013595E-07, 0.002336973833157559872, 0.004673709593152148775 ),
 .UNSPECIFIED. ) ;
#14308=DIRECTION ( 'NONE',  ( -1.000000000000000000, -4.440892098500622217E-16, 0.000000000000000000 ) ) ;
#14332=CARTESIAN_POINT ( 'NONE',  ( 8.000000000000003553, 4.618802153517037823, -0.7145311798163362926 ) ) ;
#14340=LINE ( 'NONE', #634, #18895 ) ;
#14360=CARTESIAN_POINT ( 'NONE',  ( 3.318518101603024295, 7.321656987762882096, -4.304621437946355112E-15 ) ) ;
#14389=DIRECTION ( 'NONE',  ( -1.000000000000000000, -4.440892098500622217E-16, 0.000000000000000000 ) ) ;
#14423=ORIENTED_EDGE ( 'NONE', *, *, #28249, .F. ) ;
#14445=EDGE_LOOP ( 'NONE', ( #9763, #14275, #9334, #10600, #25809, #21401 ) ) ;
#14556=CARTESIAN_POINT ( 'NONE',  ( -4.250000000000000000, -1.366904252225139372E-15, -4.449444346342715129 ) ) ;
#14579=FILL_AREA_STYLE ('',( #5748 ) ) ;
#14621=VERTEX_POINT ( 'NONE', #12429 ) ;
#14629=AXIS2_PLACEMENT_3D ( 'NONE', #23965, #24402, #12637 ) ;
#14689=EDGE_CURVE ( 'NONE', #19491, #14621, #17611, .T. ) ;
#14703=CARTESIAN_POINT ( 'NONE',  ( 0.000000000000000000, 0.000000000000000000, -5.000000000000000888 ) ) ;
#14706=CARTESIAN_POINT ( 'NONE',  ( -5.355005115540915739, -6.145890662064674714, -4.917753204360272967 ) ) ;
#14729=CARTESIAN_POINT ( 'NONE',  ( 5.000000000000006217, 2.832769448823991583E-15, -4.974599999999998801 ) ) ;
#14748=ORIENTED_EDGE ( 'NONE', *, *, #11958, .T. ) ;
#14751=ORIENTED_EDGE ( 'NONE', *, *, #3825, .F. ) ;
#14840=CARTESIAN_POINT ( 'NONE',  ( -8.000000000000000000, 4.618802153517028941, -4.285468820183664818 ) ) ;
#14850=CARTESIAN_POINT ( 'NONE',  ( -5.690023276062409430, -5.952467836904174803, -4.869346954796176519 ) ) ;
#14874=EDGE_CURVE ( 'NONE', #24756, #19707, #21283, .T. ) ;
#14883=CARTESIAN_POINT ( 'NONE',  ( 0.6543471694412491546, 8.859816792613669278, -4.503584543331193402 ) ) ;
#14912=EDGE_CURVE ( 'NONE', #6973, #27863, #6178, .T. ) ;
#14976=VECTOR ( 'NONE', #23664, 999.9999999999998863 ) ;
#15003=CIRCLE ( 'NONE', #9653, 5.000000000000005329 ) ;
#15006=CARTESIAN_POINT ( 'NONE',  ( -4.339467034331215167, -6.732211846623414431, -4.999999999999988454 ) ) ;
#15020=VERTEX_POINT ( 'NONE', #9353 ) ;
#15033=PRESENTATION_STYLE_ASSIGNMENT (( #10156 ) ) ;
#15100=DIRECTION ( 'NONE',  ( 0.000000000000000000, 0.000000000000000000, 1.000000000000000000 ) ) ;
#15101=AXIS2_PLACEMENT_3D ( 'NONE', #30103, #25464, #1839 ) ;
#15139=VERTEX_POINT ( 'NONE', #24029 ) ;
#15186=CARTESIAN_POINT ( 'NONE',  ( 8.000000000000000000, -4.618802153517027165, -0.7145311798163362926 ) ) ;
#15193=DIRECTION ( 'NONE',  ( -1.000000000000000000, -4.440892098500622217E-16, 0.000000000000000000 ) ) ;
#15232=ORIENTED_EDGE ( 'NONE', *, *, #3117, .T. ) ;
#15242=ORIENTED_EDGE ( 'NONE', *, *, #3408, .T. ) ;
#15266=CARTESIAN_POINT ( 'NONE',  ( 0.000000000000000000, 0.000000000000000000, -5.000000000000000888 ) ) ;
#15267=ORIENTED_EDGE ( 'NONE', *, *, #16094, .F. ) ;
#15335=CARTESIAN_POINT ( 'NONE',  ( 8.000000000000014211, -0.7805016046290984555, -7.137099613564734657E-15 ) ) ;
#15353=ORIENTED_EDGE ( 'NONE', *, *, #30232, .F. ) ;
#15361=B_SPLINE_CURVE_WITH_KNOTS ( 'NONE', 3,
 ( #1482, #3911, #22832, #1634, #8624, #18085 ),
 .UNSPECIFIED., .F., .F.,
 ( 4, 2, 4 ),
 ( 2.380731629606037294E-07, 0.002336973833157549030, 0.004673709593152137499 ),
 .UNSPECIFIED. ) ;
#15447=ORIENTED_EDGE ( 'NONE', *, *, #101, .F. ) ;
#15454=CARTESIAN_POINT ( 'NONE',  ( -7.999999999999996447, -3.867591403079198020, -4.502324684675412136 ) ) ;
#15461=EDGE_LOOP ( 'NONE', ( #3525, #6017, #23635, #18962, #18226, #24542 ) ) ;
#15488=VERTEX_POINT ( 'NONE', #26619 ) ;
#15502=CARTESIAN_POINT ( 'NONE',  ( 1.310872448937984602, -8.480771745766441327, -4.682649155111321626 ) ) ;
#15524=CARTESIAN_POINT ( 'NONE',  ( 5.637851296924623057E-15, 9.237604307034036566, -4.285468820183664818 ) ) ;
#15549=EDGE_LOOP ( 'NONE', ( #13308, #11638, #28700, #26377, #10701, #15563 ) ) ;
#15563=ORIENTED_EDGE ( 'NONE', *, *, #29485, .F. ) ;
#15581=AXIS2_PLACEMENT_3D ( 'NONE', #29455, #22677, #8473 ) ;
#15587=ORIENTED_EDGE ( 'NONE', *, *, #3957, .F. ) ;
#15661=EDGE_LOOP ( 'NONE', ( #29534, #28945, #20142 ) ) ;
#15698=PLANE ( 'NONE',  #29175 ) ;
#15727=DIRECTION ( 'NONE',  ( 0.000000000000000000, 0.000000000000000000, 1.000000000000000000 ) ) ;
#15773=CARTESIAN_POINT ( 'NONE',  ( 8.000000000000001776, 4.336808689942017736E-15, -5.000000000000000888 ) ) ;
#15781=VERTEX_POINT ( 'NONE', #28144 ) ;
#15887=( NAMED_UNIT ( * ) PLANE_ANGLE_UNIT ( ) SI_UNIT ( $, .RADIAN. ) );
#15941=VECTOR ( 'NONE', #24301, 1000.000000000000000 ) ;
#15970=CARTESIAN_POINT ( 'NONE',  ( -5.000000000000006217, -2.220446049250313870E-15, -4.974599999999998801 ) ) ;
#15980=ORIENTED_EDGE ( 'NONE', *, *, #18612, .F. ) ;
#15984=VECTOR ( 'NONE', #24516, 1000.000000000000000 ) ;
#16009=CARTESIAN_POINT ( 'NONE',  ( 0.000000000000000000, 0.000000000000000000, 0.000000000000000000 ) ) ;
#16094=EDGE_CURVE ( 'NONE', #1424, #19824, #18684, .T. ) ;
#16158=CONICAL_SURFACE ( 'NONE', #15101, 5.000000000000006217, 0.9599310885968819207 ) ;
#16189=CARTESIAN_POINT ( 'NONE',  ( 7.347286611336969031, 4.995646404165290377, -4.503039949738246506 ) ) ;
#16235=ORIENTED_EDGE ( 'NONE', *, *, #11616, .F. ) ;
#16300=CARTESIAN_POINT ( 'NONE',  ( -0.6527133886630267501, 8.860760056385757366, -0.4969600502617637638 ) ) ;
#16333=CARTESIAN_POINT ( 'NONE',  ( 5.355005115540903304, 6.145890662064663168, -0.08224679563972060736 ) ) ;
#16394=CARTESIAN_POINT ( 'NONE',  ( -8.000000000000001776, -4.336808689942017736E-15, 0.000000000000000000 ) ) ;
#16400=VERTEX_POINT ( 'NONE', #17508 ) ;
#16444=FACE_OUTER_BOUND ( 'NONE', #18391, .T. ) ;
#16456=DIRECTION ( 'NONE',  ( -0.5000000000000015543, 0.8660254037844378194, 0.000000000000000000 ) ) ;
#16457=CARTESIAN_POINT ( 'NONE',  ( -7.347286611336976136, -4.995646404165301036, -0.4969600502617637638 ) ) ;
#16511=ORIENTED_EDGE ( 'NONE', *, *, #4741, .F. ) ;
#16563=VERTEX_POINT ( 'NONE', #15970 ) ;
#16567=ORIENTED_EDGE ( 'NONE', *, *, #3074, .T. ) ;
#16570=DIRECTION ( 'NONE',  ( 1.000000000000000000, 4.440892098500622217E-16, 0.000000000000000000 ) ) ;
#16591=EDGE_LOOP ( 'NONE', ( #17057, #13540, #9076 ) ) ;
#16592=DIRECTION ( 'NONE',  ( -0.000000000000000000, -0.000000000000000000, -1.000000000000000000 ) ) ;
#16615=ADVANCED_FACE ( 'NONE', ( #20107 ), #11095, .F. ) ;
#16633=EDGE_LOOP ( 'NONE', ( #6732, #19267 ) ) ;
#16659=EDGE_CURVE ( 'NONE', #15488, #15781, #23453, .T. ) ;
#16750=CARTESIAN_POINT ( 'NONE',  ( 0.000000000000000000, 0.000000000000000000, 0.000000000000000000 ) ) ;
#16769=CARTESIAN_POINT ( 'NONE',  ( 8.000000000000000000, -4.618802153517025388, -5.000000000000000888 ) ) ;
#16784=CARTESIAN_POINT ( 'NONE',  ( 8.000000000000003553, 4.618802153517037823, -0.7145311798163362926 ) ) ;
#16858=DIRECTION ( 'NONE',  ( 0.000000000000000000, 0.000000000000000000, 1.000000000000000000 ) ) ;
#16888=VECTOR ( 'NONE', #12081, 1000.000000000000000 ) ;
#16961=DIRECTION ( 'NONE',  ( 0.000000000000000000, 0.000000000000000000, 1.000000000000000000 ) ) ;
#16975=CARTESIAN_POINT ( 'NONE',  ( 5.000000000000006217, 2.220446049250313870E-15, -25.03750572909317285 ) ) ;
#17000=CARTESIAN_POINT ( 'NONE',  ( 2.644994884459111795, -7.710515798486395234, -0.08224679563973184837 ) ) ;
#17012=DIRECTION ( 'NONE',  ( 1.000000000000000000, 2.220446049250312686E-15, 0.000000000000000000 ) ) ;
#17040=DIRECTION ( 'NONE',  ( 0.000000000000000000, 0.000000000000000000, -1.000000000000000000 ) ) ;
#17057=ORIENTED_EDGE ( 'NONE', *, *, #24563, .T. ) ;
#17111=CYLINDRICAL_SURFACE ( 'NONE', #13548, 5.000000000000006217 ) ;
#17126=CARTESIAN_POINT ( 'NONE',  ( 8.000000000000010658, 4.618802153517005848, -5.000000000000000888 ) ) ;
#17262=CARTESIAN_POINT ( 'NONE',  ( -4.000000000000008882, 6.928203230275508773, 0.000000000000000000 ) ) ;
#17279=EDGE_CURVE ( 'NONE', #15139, #15020, #26708, .T. ) ;
#17294=CARTESIAN_POINT ( 'NONE',  ( -6.686525924292791245, 5.377136764700170879, -4.683279549040157086 ) ) ;
#17295=CARTESIAN_POINT ( 'NONE',  ( -7.999999999999998224, -0.7805016046291067822, -5.000000000000001776 ) ) ;
#17313=DIRECTION ( 'NONE',  ( -1.000000000000000000, -4.440892098500622217E-16, 0.000000000000000000 ) ) ;
#17434=ORIENTED_EDGE ( 'NONE', *, *, #21639, .F. ) ;
#17462=DIRECTION ( 'NONE',  ( 0.000000000000000000, 0.000000000000000000, -1.000000000000000000 ) ) ;
#17483=CARTESIAN_POINT ( 'NONE',  ( 8.000000000000014211, -3.098204225878182783, -0.3157906771918849720 ) ) ;
#17508=CARTESIAN_POINT ( 'NONE',  ( -4.683753385137379155E-14, -9.237604307034027684, -0.7145311798163362926 ) ) ;
#17523=B_SPLINE_CURVE_WITH_KNOTS ( 'NONE', 3,
 ( #15186, #26833, #17483, #24518, #15335, #12037 ),
 .UNSPECIFIED., .F., .F.,
 ( 4, 2, 4 ),
 ( 0.008240550023493525833, 0.01057684187039405893, 0.01291313371729459203 ),
 .UNSPECIFIED. ) ;
#17561=CARTESIAN_POINT ( 'NONE',  ( 5.354491962338135735, -6.146186931204433712, -4.931901280394558107 ) ) ;
#17611=LINE ( 'NONE', #26652, #323 ) ;
#17642=FACE_OUTER_BOUND ( 'NONE', #27151, .T. ) ;
#17695=DIRECTION ( 'NONE',  ( 0.000000000000000000, 0.000000000000000000, -1.000000000000000000 ) ) ;
#17701=ORIENTED_EDGE ( 'NONE', *, *, #16659, .T. ) ;
#17828=FACE_OUTER_BOUND ( 'NONE', #2282, .T. ) ;
#17857=CONICAL_SURFACE ( 'NONE', #9558, 8.000000000000007105, 1.047197551196596077 ) ;
#17982=CARTESIAN_POINT ( 'NONE',  ( -7.999999999999998224, -0.7805016046291078924, 1.123165688059202250E-15 ) ) ;
#18049=VERTEX_POINT ( 'NONE', #5407 ) ;
#18085=CARTESIAN_POINT ( 'NONE',  ( 4.000000000000008882, -6.928203230275510549, 0.000000000000000000 ) ) ;
#18094=CARTESIAN_POINT ( 'NONE',  ( 2.309976723937609666, -7.903938623646900474, -4.869346954796172966 ) ) ;
#18226=ORIENTED_EDGE ( 'NONE', *, *, #16659, .F. ) ;
#18331=SHAPE_REPRESENTATION_RELATIONSHIP ( 'NONE' , 'NONE' ,  #23798, #12376 ) ;
#18345=CARTESIAN_POINT ( 'NONE',  ( 8.000000000000003553, 4.618802153517037823, -0.7145311798163362926 ) ) ;
#18391=EDGE_LOOP ( 'NONE', ( #29694, #28085, #22182, #1175 ) ) ;
#18408=ORIENTED_EDGE ( 'NONE', *, *, #12074, .F. ) ;
#18462=DIRECTION ( 'NONE',  ( 0.000000000000000000, 0.000000000000000000, 1.000000000000000000 ) ) ;
#18494=ORIENTED_EDGE ( 'NONE', *, *, #20033, .T. ) ;
#18526=MECHANICAL_DESIGN_GEOMETRIC_PRESENTATION_REPRESENTATION('',(#13160),#29292);
#18554=FACE_OUTER_BOUND ( 'NONE', #20359, .T. ) ;
#18606=EDGE_LOOP ( 'NONE', ( #10004, #12621, #10363 ) ) ;
#18612=EDGE_CURVE ( 'NONE', #6718, #14621, #19677, .T. ) ;
#18635=DIRECTION ( 'NONE',  ( 1.000000000000000000, 4.440892098500622217E-16, 0.000000000000000000 ) ) ;
#18684=B_SPLINE_CURVE_WITH_KNOTS ( 'NONE', 3,
 ( #25036, #25477, #13860, #10974, #23181, #4122, #16457, #2894 ),
 .UNSPECIFIED., .F., .F.,
 ( 4, 2, 2, 4 ),
 ( 0.004673709593152193878, 0.005837709341827673759, 0.007001709090503152773, 0.009329708587854109933 ),
 .UNSPECIFIED. ) ;
#18691=CARTESIAN_POINT ( 'NONE',  ( -8.000000000000000000, 0.7809653281575998918, 1.234974037096769500E-15 ) ) ;
#18707=ORIENTED_EDGE ( 'NONE', *, *, #17279, .T. ) ;
#18755=EDGE_CURVE ( 'NONE', #16563, #19224, #20658, .T. ) ;
#18756=DIRECTION ( 'NONE',  ( 1.000000000000000000, 4.440892098500622217E-16, 0.000000000000000000 ) ) ;
#18777=CARTESIAN_POINT ( 'NONE',  ( 5.000000000000006217, 2.832769448823991583E-15, -4.974599999999998801 ) ) ;
#18793=CIRCLE ( 'NONE', #26635, 8.000000000000005329 ) ;
#18831=AXIS2_PLACEMENT_3D ( 'NONE', #16009, #11424, #14308 ) ;
#18886=ORIENTED_EDGE ( 'NONE', *, *, #29573, .F. ) ;
#18895=VECTOR ( 'NONE', #337, 1000.000000000000000 ) ;
#18904=CONICAL_SURFACE ( 'NONE', #14026, 8.000000000000007105, 1.047197551196596077 ) ;
#18947=AXIS2_PLACEMENT_3D ( 'NONE', #26641, #5722, #7994 ) ;
#18962=ORIENTED_EDGE ( 'NONE', *, *, #29324, .F. ) ;
#19054=AXIS2_PLACEMENT_3D ( 'NONE', #8336, #3921, #4069 ) ;
#19081=FACE_OUTER_BOUND ( 'NONE', #2576, .T. ) ;
#19105=ADVANCED_FACE ( 'NONE', ( #8022 ), #21658, .F. ) ;
#19139=ORIENTED_EDGE ( 'NONE', *, *, #11899, .F. ) ;
#19149=FACE_OUTER_BOUND ( 'NONE', #10825, .T. ) ;
#19175=B_SPLINE_CURVE_WITH_KNOTS ( 'NONE', 3,
 ( #25059, #11157, #328, #27982, #9310, #5193, #16189, #12054 ),
 .UNSPECIFIED., .F., .F.,
 ( 4, 2, 2, 4 ),
 ( 0.004673709593152178265, 0.005837709341827659881, 0.007001709090503141497, 0.009329708587854104729 ),
 .UNSPECIFIED. ) ;
#19219=ORIENTED_EDGE ( 'NONE', *, *, #12074, .T. ) ;
#19224=VERTEX_POINT ( 'NONE', #14729 ) ;
#19247=CARTESIAN_POINT ( 'NONE',  ( -5.354491962338132183, 6.146186931204415949, -0.06809871960543412150 ) ) ;
#19254=LINE ( 'NONE', #16975, #22782 ) ;
#19267=ORIENTED_EDGE ( 'NONE', *, *, #30047, .F. ) ;
#19460=VECTOR ( 'NONE', #12521, 1000.000000000000000 ) ;
#19491=VERTEX_POINT ( 'NONE', #25874 ) ;
#19498=PRODUCT_DEFINITION_FORMATION_WITH_SPECIFIED_SOURCE ( 'ANY', '', #28886, .NOT_KNOWN. ) ;
#19541=DIRECTION ( 'NONE',  ( 0.000000000000000000, 0.000000000000000000, 1.000000000000000000 ) ) ;
#19606=DIRECTION ( 'NONE',  ( 0.000000000000000000, 0.000000000000000000, 1.000000000000000000 ) ) ;
#19677=CIRCLE ( 'NONE', #2641, 4.250000000000003553 ) ;
#19685=B_SPLINE_CURVE_WITH_KNOTS ( 'NONE', 3,
 ( #26959, #15006, #5572, #14706, #14850, #24635, #24194, #12571 ),
 .UNSPECIFIED., .F., .F.,
 ( 4, 2, 2, 4 ),
 ( 0.004673709593152193878, 0.005837709341827673759, 0.007001709090503152773, 0.009329708587854109933 ),
 .UNSPECIFIED. ) ;
#19698=ORIENTED_EDGE ( 'NONE', *, *, #24948, .T. ) ;
#19707=VERTEX_POINT ( 'NONE', #23576 ) ;
#19752=CARTESIAN_POINT ( 'NONE',  ( 0.000000000000000000, 0.000000000000000000, -5.000000000000000888 ) ) ;
#19759=AXIS2_PLACEMENT_3D ( 'NONE', #20226, #24828, #6204 ) ;
#19782=CONICAL_SURFACE ( 'NONE', #10039, 8.000000000000007105, 1.047197551196596077 ) ;
#19794=B_SPLINE_CURVE_WITH_KNOTS ( 'NONE', 3,
 ( #7690, #24327, #989, #17000, #678, #540, #9823, #7545 ),
 .UNSPECIFIED., .F., .F.,
 ( 4, 2, 2, 4 ),
 ( 0.004673709593152137499, 0.005837709341827637330, 0.007001709090503138028, 0.009329708587854137689 ),
 .UNSPECIFIED. ) ;
#19800=ORIENTED_EDGE ( 'NONE', *, *, #26054, .T. ) ;
#19804=CONICAL_SURFACE ( 'NONE', #18831, 8.000000000000007105, 1.047197551196596077 ) ;
#19824=VERTEX_POINT ( 'NONE', #832 ) ;
#19938=DIRECTION ( 'NONE',  ( 0.000000000000000000, -0.000000000000000000, 1.000000000000000000 ) ) ;
#19978=CARTESIAN_POINT ( 'NONE',  ( 8.000000000000001776, 4.336808689942017736E-15, 0.000000000000000000 ) ) ;
#20033=EDGE_CURVE ( 'NONE', #19224, #16563, #29030, .T. ) ;
#20107=FACE_OUTER_BOUND ( 'NONE', #21762, .T. ) ;
#20128=CARTESIAN_POINT ( 'NONE',  ( 5.000000000000006217, 2.220446049250313870E-15, -5.000000000000000888 ) ) ;
#20142=ORIENTED_EDGE ( 'NONE', *, *, #138, .F. ) ;
#20155=FACE_OUTER_BOUND ( 'NONE', #10857, .T. ) ;
#20208=EDGE_CURVE ( 'NONE', #12491, #13323, #12894, .T. ) ;
#20211=DIRECTION ( 'NONE',  ( 1.000000000000000000, 4.440892098500622217E-16, 0.000000000000000000 ) ) ;
#20216=B_SPLINE_CURVE_WITH_KNOTS ( 'NONE', 3,
 ( #22624, #21182, #25475, #145, #4710, #445, #16300, #4566 ),
 .UNSPECIFIED., .F., .F.,
 ( 4, 2, 2, 4 ),
 ( 0.004673709593152147908, 0.005837709341827640799, 0.007001709090503132824, 0.009329708587854118607 ),
 .UNSPECIFIED. ) ;
#20226=CARTESIAN_POINT ( 'NONE',  ( -8.000000000000003553, -4.618802153517028941, -5.000000000000000888 ) ) ;
#20295=AXIS2_PLACEMENT_3D ( 'NONE', #19752, #29122, #8162 ) ;
#20304=FACE_BOUND ( 'NONE', #16633, .T. ) ;
#20316=( NAMED_UNIT ( * ) SI_UNIT ( $, .STERADIAN. ) SOLID_ANGLE_UNIT ( ) );
#20330=DIRECTION ( 'NONE',  ( 0.000000000000000000, 0.000000000000000000, 1.000000000000000000 ) ) ;
#20359=EDGE_LOOP ( 'NONE', ( #26735, #26726, #10608, #15980 ) ) ;
#20380=CARTESIAN_POINT ( 'NONE',  ( 4.000000000000008882, -6.928203230275510549, -5.000000000000000888 ) ) ;
#20532=CARTESIAN_POINT ( 'NONE',  ( -4.683753385137379155E-14, -9.237604307034027684, -4.285468820183664818 ) ) ;
#20607=DIRECTION ( 'NONE',  ( 0.000000000000000000, 0.000000000000000000, 1.000000000000000000 ) ) ;
#20658=CIRCLE ( 'NONE', #7508, 5.000000000000006217 ) ;
#20692=CARTESIAN_POINT ( 'NONE',  ( -2.309976723937612331, 7.903938623646880046, -4.869346954796183624 ) ) ;
#20716=EDGE_LOOP ( 'NONE', ( #5661, #15242, #10073, #15587, #18886, #922 ) ) ;
#20779=PRODUCT_DEFINITION_CONTEXT ( 'detailed design', #1518, 'design' ) ;
#20873=EDGE_LOOP ( 'NONE', ( #19139, #13690, #15267 ) ) ;
#21062=ADVANCED_FACE ( 'NONE', ( #10777 ), #8775, .T. ) ;
#21172=DIRECTION ( 'NONE',  ( 1.000000000000000000, 4.440892098500622217E-16, 0.000000000000000000 ) ) ;
#21182=CARTESIAN_POINT ( 'NONE',  ( -3.660532965668823913, 7.124194613927632425, -2.285083133455287951E-15 ) ) ;
#21183=AXIS2_PLACEMENT_3D ( 'NONE', #26951, #20330, #29717 ) ;
#21283=CIRCLE ( 'NONE', #28629, 8.000000000000005329 ) ;
#21344=EDGE_CURVE ( 'NONE', #27863, #15139, #18793, .T. ) ;
#21367=CARTESIAN_POINT ( 'NONE',  ( 5.690023276062400548, 5.952467836904161480, -0.1306530452038157097 ) ) ;
#21401=ORIENTED_EDGE ( 'NONE', *, *, #10659, .F. ) ;
#21467=DIRECTION ( 'NONE',  ( -1.000000000000000000, -4.440892098500622217E-16, 0.000000000000000000 ) ) ;
#21477=ADVANCED_FACE ( 'NONE', ( #551 ), #19782, .T. ) ;
#21484=ORIENTED_EDGE ( 'NONE', *, *, #25576, .T. ) ;
#21498=CONICAL_SURFACE ( 'NONE', #8361, 8.000000000000007105, 1.047197551196596077 ) ;
#21528=VECTOR ( 'NONE', #15727, 1000.000000000000000 ) ;
#21639=EDGE_CURVE ( 'NONE', #29239, #1679, #12481, .T. ) ;
#21658=CONICAL_SURFACE ( 'NONE', #22635, 5.000000000000006217, 0.9599310885968819207 ) ;
#21707=CARTESIAN_POINT ( 'NONE',  ( -5.000000000000005329, -1.608122649676636157E-15, 0.000000000000000000 ) ) ;
#21718=EDGE_CURVE ( 'NONE', #12491, #24756, #10527, .T. ) ;
#21762=EDGE_LOOP ( 'NONE', ( #14748, #1816, #211, #16235 ) ) ;
#21768=SURFACE_STYLE_FILL_AREA ( #14579 ) ;
#21770=CARTESIAN_POINT ( 'NONE',  ( 0.000000000000000000, 0.000000000000000000, -4.974599999999998801 ) ) ;
#21907=VECTOR ( 'NONE', #25985, 1000.000000000000000 ) ;
#21927=( GEOMETRIC_REPRESENTATION_CONTEXT ( 3 ) GLOBAL_UNCERTAINTY_ASSIGNED_CONTEXT ( ( #1596 ) ) GLOBAL_UNIT_ASSIGNED_CONTEXT ( ( #3021, #10003, #12600 ) ) REPRESENTATION_CONTEXT ( 'NONE', 'WORKASPACE' ) );
#21932=ADVANCED_FACE ( 'NONE', ( #8391 ), #17857, .T. ) ;
#22035=ADVANCED_FACE ( 'NONE', ( #11725 ), #19804, .T. ) ;
#22053=LINE ( 'NONE', #26808, #24686 ) ;
#22182=ORIENTED_EDGE ( 'NONE', *, *, #29927, .F. ) ;
#22283=EDGE_CURVE ( 'NONE', #15020, #8203, #9482, .T. ) ;
#22322=CARTESIAN_POINT ( 'NONE',  ( 8.000000000000015987, -1.555946510856142551, -4.932911297836637843 ) ) ;
#22374=AXIS2_PLACEMENT_3D ( 'NONE', #2459, #18462, #27815 ) ;
#22413=DIRECTION ( 'NONE',  ( 1.000000000000000000, 4.440892098500622217E-16, 0.000000000000000000 ) ) ;
#22415=MECHANICAL_DESIGN_GEOMETRIC_PRESENTATION_REPRESENTATION('',(#14118),#21927);
#22417=EDGE_CURVE ( 'NONE', #18049, #24756, #8688, .T. ) ;
#22458=EDGE_CURVE ( 'NONE', #2266, #6973, #28751, .T. ) ;
#22490=CARTESIAN_POINT ( 'NONE',  ( -7.999999999999998224, -3.098204225878191664, -4.684209322808124298 ) ) ;
#22584=CARTESIAN_POINT ( 'NONE',  ( 0.000000000000000000, 0.000000000000000000, -5.000000000000000888 ) ) ;
#22624=CARTESIAN_POINT ( 'NONE',  ( -4.000000000000008882, 6.928203230275508773, 0.000000000000000000 ) ) ;
#22635=AXIS2_PLACEMENT_3D ( 'NONE', #21770, #17040, #21467 ) ;
#22677=DIRECTION ( 'NONE',  ( 0.5000000000000017764, 0.8660254037844375974, 0.000000000000000000 ) ) ;
#22717=CARTESIAN_POINT ( 'NONE',  ( -8.000000000000000000, 3.871967595402115769, -0.4989386132324554746 ) ) ;
#22733=DIRECTION ( 'NONE',  ( 0.000000000000000000, 0.000000000000000000, 1.000000000000000000 ) ) ;
#22735=CARTESIAN_POINT ( 'NONE',  ( -8.000000000000001776, -4.336808689942017736E-15, 0.000000000000000000 ) ) ;
#22736=ORIENTED_EDGE ( 'NONE', *, *, #3117, .F. ) ;
#22782=VECTOR ( 'NONE', #23550, 1000.000000000000000 ) ;
#22832=CARTESIAN_POINT ( 'NONE',  ( 6.686525924292798351, -5.377136764700183313, -0.3167204509598521289 ) ) ;
#22944=CARTESIAN_POINT ( 'NONE',  ( 8.000000000000010658, 3.871967595402145967, -0.4989386132324691303 ) ) ;
#22992=CARTESIAN_POINT ( 'NONE',  ( -0.6543471694412856809, -8.859816792613662173, -4.503584543331194290 ) ) ;
#23139=CARTESIAN_POINT ( 'NONE',  ( 4.000000000000008882, -6.928203230275510549, -5.000000000000000888 ) ) ;
#23140=ADVANCED_FACE ( 'NONE', ( #1645, #17642 ), #3622, .T. ) ;
#23151=CARTESIAN_POINT ( 'NONE',  ( -7.999999999999998224, 3.871967595402137974, -4.501061386767540640 ) ) ;
#23181=CARTESIAN_POINT ( 'NONE',  ( -5.690023276062409430, -5.952467836904174803, -0.1306530452038248968 ) ) ;
#23225=ORIENTED_EDGE ( 'NONE', *, *, #28249, .T. ) ;
#23238=CARTESIAN_POINT ( 'NONE',  ( 2.645508037661891354, 7.710219529346620249, -0.06809871960543666114 ) ) ;
#23304=DIRECTION ( 'NONE',  ( 0.000000000000000000, 0.000000000000000000, 1.000000000000000000 ) ) ;
#23319=DIRECTION ( 'NONE',  ( 0.000000000000000000, 0.000000000000000000, 1.000000000000000000 ) ) ;
#23320=DIRECTION ( 'NONE',  ( 1.000000000000000000, 4.440892098500622217E-16, 0.000000000000000000 ) ) ;
#23330=DIRECTION ( 'NONE',  ( -0.8660254037844377084, -0.5000000000000014433, 0.000000000000000000 ) ) ;
#23453=B_SPLINE_CURVE_WITH_KNOTS ( 'NONE', 3,
 ( #2115, #10940, #11387, #29936, #20692, #9090, #24699, #15524 ),
 .UNSPECIFIED., .F., .F.,
 ( 4, 2, 2, 4 ),
 ( 0.004673709593152148775, 0.005837709341827642534, 0.007001709090503135426, 0.009329708587854122076 ),
 .UNSPECIFIED. ) ;
#23525=VERTEX_POINT ( 'NONE', #7711 ) ;
#23530=B_SPLINE_CURVE_WITH_KNOTS ( 'NONE', 3,
 ( #5994, #24613, #6293, #22322, #10408, #3270 ),
 .UNSPECIFIED., .F., .F.,
 ( 4, 2, 4 ),
 ( 0.008240550023493525833, 0.01057684187039405893, 0.01291313371729459203 ),
 .UNSPECIFIED. ) ;
#23536=LINE ( 'NONE', #7506, #953 ) ;
#23550=DIRECTION ( 'NONE',  ( 0.000000000000000000, 0.000000000000000000, 1.000000000000000000 ) ) ;
#23576=CARTESIAN_POINT ( 'NONE',  ( -4.000000000000008882, 6.928203230275508773, 0.000000000000000000 ) ) ;
#23581=ORIENTED_EDGE ( 'NONE', *, *, #26991, .T. ) ;
#23635=ORIENTED_EDGE ( 'NONE', *, *, #138, .T. ) ;
#23664=DIRECTION ( 'NONE',  ( 0.8191520442889924647, 4.640937770007144753E-16, -0.5735764363510452712 ) ) ;
#23666=DIRECTION ( 'NONE',  ( 0.000000000000000000, 0.000000000000000000, 1.000000000000000000 ) ) ;
#23686=EDGE_CURVE ( 'NONE', #14621, #23525, #22053, .T. ) ;
#23761=CIRCLE ( 'NONE', #10587, 8.000000000000005329 ) ;
#23777=ORIENTED_EDGE ( 'NONE', *, *, #3074, .F. ) ;
#23798=SHAPE_REPRESENTATION ( 'hex thin nut chamfered gradeab_iso_ISO - 4035 - M10 - N', ( #13190 ), #496 ) ;
#23842=DIRECTION ( 'NONE',  ( 1.000000000000000000, 4.440892098500622217E-16, 0.000000000000000000 ) ) ;
#23849=DIRECTION ( 'NONE',  ( -1.000000000000000000, -4.440892098500622217E-16, 0.000000000000000000 ) ) ;
#23939=CARTESIAN_POINT ( 'NONE',  ( 8.000000000000001776, 4.336808689942017736E-15, -5.000000000000000888 ) ) ;
#23941=CONICAL_SURFACE ( 'NONE', #4902, 8.000000000000007105, 1.047197551196596077 ) ;
#23965=CARTESIAN_POINT ( 'NONE',  ( 0.000000000000000000, 0.000000000000000000, -5.000000000000000888 ) ) ;
#23983=CARTESIAN_POINT ( 'NONE',  ( 4.000000000000019540, 6.928203230275512325, 0.000000000000000000 ) ) ;
#24029=CARTESIAN_POINT ( 'NONE',  ( -8.000000000000001776, -4.336808689942017736E-15, -5.000000000000000888 ) ) ;
#24046=DIRECTION ( 'NONE',  ( -0.000000000000000000, -0.000000000000000000, -1.000000000000000000 ) ) ;
#24177=CARTESIAN_POINT ( 'NONE',  ( -4.681481898397004571, 6.534749472788154101, -5.000000000000000000 ) ) ;
#24194=CARTESIAN_POINT ( 'NONE',  ( -7.347286611336976136, -4.995646404165301036, -4.503039949738237624 ) ) ;
#24231=CARTESIAN_POINT ( 'NONE',  ( 6.505213034913026604E-15, 9.237604307034033013, -5.000000000000000888 ) ) ;
#24236=FACE_OUTER_BOUND ( 'NONE', #5495, .T. ) ;
#24301=DIRECTION ( 'NONE',  ( 0.000000000000000000, 0.000000000000000000, 1.000000000000000000 ) ) ;
#24327=CARTESIAN_POINT ( 'NONE',  ( 3.660532965668829686, -7.124194613927648412, -1.188556631587234551E-14 ) ) ;
#24359=CIRCLE ( 'NONE', #3877, 8.000000000000005329 ) ;
#24376=LINE ( 'NONE', #24231, #6836 ) ;
#24400=EDGE_LOOP ( 'NONE', ( #28092, #8546, #3540 ) ) ;
#24402=DIRECTION ( 'NONE',  ( -0.000000000000000000, -0.000000000000000000, -1.000000000000000000 ) ) ;
#24430=CIRCLE ( 'NONE', #19054, 4.250000000000003553 ) ;
#24451=DIRECTION ( 'NONE',  ( 1.000000000000000000, 4.440892098500622217E-16, 0.000000000000000000 ) ) ;
#24476=CARTESIAN_POINT ( 'NONE',  ( -8.000000000000001776, -4.336808689942017736E-15, -5.000000000000000888 ) ) ;
#24516=DIRECTION ( 'NONE',  ( -0.8191520442889943521, -2.634593911900098464E-16, 0.5735764363510424957 ) ) ;
#24518=CARTESIAN_POINT ( 'NONE',  ( 8.000000000000015987, -1.555946510856143883, -0.06708870216336296211 ) ) ;
#24536=CARTESIAN_POINT ( 'NONE',  ( 0.000000000000000000, 0.000000000000000000, -5.000000000000000888 ) ) ;
#24542=ORIENTED_EDGE ( 'NONE', *, *, #2314, .F. ) ;
#24563=EDGE_CURVE ( 'NONE', #1679, #26232, #19175, .T. ) ;
#24589=LINE ( 'NONE', #3681, #19460 ) ;
#24613=CARTESIAN_POINT ( 'NONE',  ( 8.000000000000014211, -3.867591403079186030, -4.502324684675405031 ) ) ;
#24635=CARTESIAN_POINT ( 'NONE',  ( -6.689127551062014732, -5.375634714784644608, -4.682649155111332284 ) ) ;
#24659=EDGE_CURVE ( 'NONE', #24756, #13323, #10451, .T. ) ;
#24686=VECTOR ( 'NONE', #26496, 1000.000000000000000 ) ;
#24699=CARTESIAN_POINT ( 'NONE',  ( -0.6527133886630255288, 8.860760056385759142, -4.503039949738237624 ) ) ;
#24700=ADVANCED_FACE ( 'NONE', ( #19081 ), #10064, .F. ) ;
#24711=CARTESIAN_POINT ( 'NONE',  ( 0.000000000000000000, 0.000000000000000000, -4.974599999999998801 ) ) ;
#24756=VERTEX_POINT ( 'NONE', #23983 ) ;
#24773=CIRCLE ( 'NONE', #26722, 8.000000000000005329 ) ;
#24828=DIRECTION ( 'NONE',  ( -0.5000000000000017764, -0.8660254037844377084, 0.000000000000000000 ) ) ;
#24833=CARTESIAN_POINT ( 'NONE',  ( 0.6527133886630124282, -8.860760056385789341, -4.503039949738222525 ) ) ;
#24839=CARTESIAN_POINT ( 'NONE',  ( 0.000000000000000000, 0.000000000000000000, 0.000000000000000000 ) ) ;
#24948=EDGE_CURVE ( 'NONE', #19824, #28625, #1714, .T. ) ;
#24955=VERTEX_POINT ( 'NONE', #20128 ) ;
#24962=CARTESIAN_POINT ( 'NONE',  ( 8.000000000000008882, 3.871967595402145967, -4.501061386767531758 ) ) ;
#24992=ADVANCED_FACE ( 'NONE', ( #3968 ), #9098, .T. ) ;
#25036=CARTESIAN_POINT ( 'NONE',  ( -4.000000000000020428, -6.928203230275511437, 0.000000000000000000 ) ) ;
#25059=CARTESIAN_POINT ( 'NONE',  ( 4.000000000000019540, 6.928203230275512325, -5.000000000000000888 ) ) ;
#25066=( LENGTH_UNIT ( ) NAMED_UNIT ( * ) SI_UNIT ( .MILLI., .METRE. ) );
#25099=CARTESIAN_POINT ( 'NONE',  ( 8.000000000000012434, 0.7809653281576151018, -4.999999999999993783 ) ) ;
#25167=CONICAL_SURFACE ( 'NONE', #11986, 8.000000000000007105, 1.047197551196596077 ) ;
#25221=( LENGTH_UNIT ( ) NAMED_UNIT ( * ) SI_UNIT ( .MILLI., .METRE. ) );
#25265=PLANE ( 'NONE',  #15581 ) ;
#25293=CONICAL_SURFACE ( 'NONE', #18947, 8.000000000000007105, 1.047197551196596077 ) ;
#25362=ORIENTED_EDGE ( 'NONE', *, *, #14270, .T. ) ;
#25366=SHAPE_DEFINITION_REPRESENTATION ( #3755, #23798 ) ;
#25464=DIRECTION ( 'NONE',  ( 0.000000000000000000, 0.000000000000000000, -1.000000000000000000 ) ) ;
#25475=CARTESIAN_POINT ( 'NONE',  ( -3.319543390096041602, 7.321065037175435108, -0.01688885742777280694 ) ) ;
#25477=CARTESIAN_POINT ( 'NONE',  ( -4.339467034331215167, -6.732211846623414431, -1.342271935690208390E-14 ) ) ;
#25519=AXIS2_PLACEMENT_3D ( 'NONE', #29949, #2130, #8817 ) ;
#25576=EDGE_CURVE ( 'NONE', #29239, #26232, #2796, .T. ) ;
#25584=CARTESIAN_POINT ( 'NONE',  ( -8.000000000000000000, 0.7809653281576059980, -5.000000000000003553 ) ) ;
#25704=ORIENTED_EDGE ( 'NONE', *, *, #30047, .T. ) ;
#25769=ORIENTED_EDGE ( 'NONE', *, *, #101, .T. ) ;
#25809=ORIENTED_EDGE ( 'NONE', *, *, #24563, .F. ) ;
#25870=CARTESIAN_POINT ( 'NONE',  ( 0.000000000000000000, 0.000000000000000000, 0.000000000000000000 ) ) ;
#25874=CARTESIAN_POINT ( 'NONE',  ( 4.250000000000000000, 1.887379141862764541E-15, -4.449444346342715129 ) ) ;
#25917=DIRECTION ( 'NONE',  ( 1.000000000000000000, -1.332267629550188046E-15, 0.000000000000000000 ) ) ;
#25978=AXIS2_PLACEMENT_3D ( 'NONE', #13242, #27615, #4385 ) ;
#25985=DIRECTION ( 'NONE',  ( 0.000000000000000000, 0.000000000000000000, 1.000000000000000000 ) ) ;
#26054=EDGE_CURVE ( 'NONE', #15139, #15488, #24773, .T. ) ;
#26068=VERTEX_POINT ( 'NONE', #21707 ) ;
#26085=DIRECTION ( 'NONE',  ( 0.000000000000000000, 0.000000000000000000, 1.000000000000000000 ) ) ;
#26232=VERTEX_POINT ( 'NONE', #29549 ) ;
#26287=DIRECTION ( 'NONE',  ( 1.000000000000000000, 4.440892098500622217E-16, 0.000000000000000000 ) ) ;
#26288=LINE ( 'NONE', #2791, #21907 ) ;
#26294=CARTESIAN_POINT ( 'NONE',  ( 6.686525924292798351, -5.377136764700186866, -4.683279549040149092 ) ) ;
#26307=CLOSED_SHELL ( 'NONE', ( #16615, #4018, #3547, #13859, #6951, #268, #1934, #2109, #10311, #21062, #12513, #23140, #6266, #2937, #4402, #27516, #24992, #4197, #11283, #7118, #22035, #2145, #2887, #21477, #21932, #24700, #19105, #13104 ) ) ;
#26327=CARTESIAN_POINT ( 'NONE',  ( 8.000000000000000000, -4.618802153517027165, -4.285468820183664818 ) ) ;
#26363=EDGE_CURVE ( 'NONE', #6624, #16563, #14340, .T. ) ;
#26377=ORIENTED_EDGE ( 'NONE', *, *, #28242, .F. ) ;
#26399=CONICAL_SURFACE ( 'NONE', #5917, 8.000000000000007105, 1.047197551196596077 ) ;
#26409=ORIENTED_EDGE ( 'NONE', *, *, #1549, .T. ) ;
#26439=DIRECTION ( 'NONE',  ( 0.000000000000000000, 0.000000000000000000, 1.000000000000000000 ) ) ;
#26496=DIRECTION ( 'NONE',  ( 0.8191520442889943521, 3.637765840953626539E-16, 0.5735764363510424957 ) ) ;
#26568=EDGE_LOOP ( 'NONE', ( #9947, #6670, #18707 ) ) ;
#26619=CARTESIAN_POINT ( 'NONE',  ( -4.000000000000008882, 6.928203230275508773, -5.000000000000000888 ) ) ;
#26635=AXIS2_PLACEMENT_3D ( 'NONE', #14703, #24046, #17012 ) ;
#26640=CARTESIAN_POINT ( 'NONE',  ( 0.000000000000000000, 0.000000000000000000, 0.000000000000000000 ) ) ;
#26641=CARTESIAN_POINT ( 'NONE',  ( 0.000000000000000000, 0.000000000000000000, -5.000000000000000888 ) ) ;
#26652=CARTESIAN_POINT ( 'NONE',  ( 4.250000000000003553, 1.887379141862766119E-15, -5.000000000000000888 ) ) ;
#26708=B_SPLINE_CURVE_WITH_KNOTS ( 'NONE', 3,
 ( #11842, #25584, #27620, #4830, #23151, #7127 ),
 .UNSPECIFIED., .F., .F.,
 ( 4, 2, 4 ),
 ( 0.01291313371729458509, 0.01525081363757310911, 0.01758849355785163313 ),
 .UNSPECIFIED. ) ;
#26722=AXIS2_PLACEMENT_3D ( 'NONE', #27082, #3858, #29232 ) ;
#26726=ORIENTED_EDGE ( 'NONE', *, *, #10661, .F. ) ;
#26735=ORIENTED_EDGE ( 'NONE', *, *, #28526, .F. ) ;
#26808=CARTESIAN_POINT ( 'NONE',  ( 4.175000000000003375, 1.854072451124011344E-15, -0.5776712190230064436 ) ) ;
#26833=CARTESIAN_POINT ( 'NONE',  ( 8.000000000000014211, -3.867591403079187806, -0.4976753153245951355 ) ) ;
#26845=COLOUR_RGB ( '', 0.31764706, 0.68627451, 0.89019608) ;
#26913=CARTESIAN_POINT ( 'NONE',  ( 4.000000000000008882, -6.928203230275510549, -5.000000000000000888 ) ) ;
#26951=CARTESIAN_POINT ( 'NONE',  ( 0.000000000000000000, 0.000000000000000000, -4.974599999999998801 ) ) ;
#26959=CARTESIAN_POINT ( 'NONE',  ( -4.000000000000020428, -6.928203230275511437, -5.000000000000000888 ) ) ;
#26991=EDGE_CURVE ( 'NONE', #26068, #23525, #15003, .T. ) ;
#26999=DIRECTION ( 'NONE',  ( 1.000000000000000000, 4.440892098500622217E-16, 0.000000000000000000 ) ) ;
#27006=DIRECTION ( 'NONE',  ( 1.000000000000000000, 4.440892098500622217E-16, 0.000000000000000000 ) ) ;
#27043=CARTESIAN_POINT ( 'NONE',  ( -7.999999999999998224, -3.098204225878192997, -0.3157906771918777000 ) ) ;
#27082=CARTESIAN_POINT ( 'NONE',  ( 0.000000000000000000, 0.000000000000000000, -5.000000000000000888 ) ) ;
#27085=( NAMED_UNIT ( * ) SI_UNIT ( $, .STERADIAN. ) SOLID_ANGLE_UNIT ( ) );
#27147=CARTESIAN_POINT ( 'NONE',  ( 2.644994884459111351, -7.710515798486395234, -4.917753204360269415 ) ) ;
#27151=EDGE_LOOP ( 'NONE', ( #26409, #27995, #8732, #9806, #28217, #16567 ) ) ;
#27516=ADVANCED_FACE ( 'NONE', ( #12871 ), #25293, .T. ) ;
#27542=SURFACE_SIDE_STYLE ('',( #6595 ) ) ;
#27552=CARTESIAN_POINT ( 'NONE',  ( 8.000000000000001776, 4.336808689942017736E-15, 0.000000000000000000 ) ) ;
#27575=EDGE_LOOP ( 'NONE', ( #971, #19698, #13871, #12921, #12847, #2551 ) ) ;
#27615=DIRECTION ( 'NONE',  ( 0.000000000000000000, 0.000000000000000000, 1.000000000000000000 ) ) ;
#27620=CARTESIAN_POINT ( 'NONE',  ( -7.999999999999998224, 1.572549600175623841, -4.931055444744870009 ) ) ;
#27647=AXIS2_PLACEMENT_3D ( 'NONE', #24839, #1047, #10324 ) ;
#27655=APPLICATION_CONTEXT ( 'automotive_design' ) ;
#27751=CARTESIAN_POINT ( 'NONE',  ( -3.318518101603040726, -7.321656987762888313, -4.999999999999986677 ) ) ;
#27774=CARTESIAN_POINT ( 'NONE',  ( -4.000000000000020428, -6.928203230275511437, 0.000000000000000000 ) ) ;
#27783=CARTESIAN_POINT ( 'NONE',  ( 0.000000000000000000, 0.000000000000000000, -5.000000000000000888 ) ) ;
#27785=B_SPLINE_CURVE_WITH_KNOTS ( 'NONE', 3,
 ( #20532, #22992, #6509, #13366, #27751, #13668 ),
 .UNSPECIFIED., .F., .F.,
 ( 4, 2, 4 ),
 ( 2.380731630115636932E-07, 0.002336973833157603240, 0.004673709593152193878 ),
 .UNSPECIFIED. ) ;
#27803=EDGE_CURVE ( 'NONE', #4596, #15139, #7435, .T. ) ;
#27815=DIRECTION ( 'NONE',  ( 1.000000000000000000, 4.440892098500622217E-16, 0.000000000000000000 ) ) ;
#27818=ORIENTED_EDGE ( 'NONE', *, *, #12725, .F. ) ;
#27863=VERTEX_POINT ( 'NONE', #8136 ) ;
#27982=CARTESIAN_POINT ( 'NONE',  ( 5.355005115540903304, 6.145890662064663168, -4.917753204360280961 ) ) ;
#27995=ORIENTED_EDGE ( 'NONE', *, *, #21718, .T. ) ;
#28038=CARTESIAN_POINT ( 'NONE',  ( -8.000000000000000000, 4.618802153517001408, -0.7145311798163294092 ) ) ;
#28085=ORIENTED_EDGE ( 'NONE', *, *, #28526, .T. ) ;
#28092=ORIENTED_EDGE ( 'NONE', *, *, #21718, .F. ) ;
#28096=FACE_OUTER_BOUND ( 'NONE', #15461, .T. ) ;
#28116=AXIS2_PLACEMENT_3D ( 'NONE', #7249, #13793, #7403 ) ;
#28133=CARTESIAN_POINT ( 'NONE',  ( 4.000000000000019540, 6.928203230275512325, 0.000000000000000000 ) ) ;
#28144=CARTESIAN_POINT ( 'NONE',  ( 5.637851296924623057E-15, 9.237604307034036566, -4.285468820183664818 ) ) ;
#28217=ORIENTED_EDGE ( 'NONE', *, *, #11899, .T. ) ;
#28235=ORIENTED_EDGE ( 'NONE', *, *, #3825, .T. ) ;
#28242=EDGE_CURVE ( 'NONE', #4596, #19824, #26288, .T. ) ;
#28249=EDGE_CURVE ( 'NONE', #5542, #16563, #23536, .T. ) ;
#28387=AXIS2_PLACEMENT_3D ( 'NONE', #11964, #16858, #9521 ) ;
#28526=EDGE_CURVE ( 'NONE', #5542, #6718, #24589, .T. ) ;
#28625=VERTEX_POINT ( 'NONE', #8845 ) ;
#28629=AXIS2_PLACEMENT_3D ( 'NONE', #10897, #13045, #20211 ) ;
#28657=ORIENTED_EDGE ( 'NONE', *, *, #26363, .F. ) ;
#28700=ORIENTED_EDGE ( 'NONE', *, *, #16094, .T. ) ;
#28751=B_SPLINE_CURVE_WITH_KNOTS ( 'NONE', 3,
 ( #10238, #1253, #26294, #17561, #7813, #26913 ),
 .UNSPECIFIED., .F., .F.,
 ( 4, 2, 4 ),
 ( 2.380731629605729715E-07, 0.002336973833157549897, 0.004673709593152139234 ),
 .UNSPECIFIED. ) ;
#28761=FACE_OUTER_BOUND ( 'NONE', #12636, .T. ) ;
#28886=PRODUCT ( 'hex thin nut chamfered gradeab_iso_ISO - 4035 - M10 - N', 'hex thin nut chamfered gradeab_iso_ISO - 4035 - M10 - N', '', ( #6750 ) ) ;
#28945=ORIENTED_EDGE ( 'NONE', *, *, #22417, .F. ) ;
#28948=CARTESIAN_POINT ( 'NONE',  ( -5.354491962338129518, 6.146186931204416837, -4.931901280394566989 ) ) ;
#28985=CARTESIAN_POINT ( 'NONE',  ( -4.175000000000003375, -1.342782412479990996E-15, -0.5776712190230064436 ) ) ;
#28999=CARTESIAN_POINT ( 'NONE',  ( -5.000000000000001776, -1.608122649676635171E-15, -5.000000000000000888 ) ) ;
#29030=CIRCLE ( 'NONE', #21183, 5.000000000000006217 ) ;
#29074=AXIS2_PLACEMENT_3D ( 'NONE', #1339, #19938, #26999 ) ;
#29093=CARTESIAN_POINT ( 'NONE',  ( 4.000000000000008882, -6.928203230275510549, 0.000000000000000000 ) ) ;
#29122=DIRECTION ( 'NONE',  ( -0.000000000000000000, -0.000000000000000000, -1.000000000000000000 ) ) ;
#29175=AXIS2_PLACEMENT_3D ( 'NONE', #4113, #13407, #22733 ) ;
#29195=B_SPLINE_CURVE_WITH_KNOTS ( 'NONE', 3,
 ( #16394, #18691, #1519, #13391, #22717, #28038 ),
 .UNSPECIFIED., .F., .F.,
 ( 4, 2, 4 ),
 ( 0.01291313371729458682, 0.01525081363757309696, 0.01758849355785160884 ),
 .UNSPECIFIED. ) ;
#29199=CARTESIAN_POINT ( 'NONE',  ( 0.000000000000000000, 0.000000000000000000, 0.000000000000000000 ) ) ;
#29224=ORIENTED_EDGE ( 'NONE', *, *, #1549, .F. ) ;
#29232=DIRECTION ( 'NONE',  ( 1.000000000000000000, 2.220446049250312686E-15, 0.000000000000000000 ) ) ;
#29239=VERTEX_POINT ( 'NONE', #23939 ) ;
#29253=EDGE_CURVE ( 'NONE', #19707, #28625, #4389, .T. ) ;
#29265=FACE_OUTER_BOUND ( 'NONE', #5828, .T. ) ;
#29292=( GEOMETRIC_REPRESENTATION_CONTEXT ( 3 ) GLOBAL_UNCERTAINTY_ASSIGNED_CONTEXT ( ( #11919 ) ) GLOBAL_UNIT_ASSIGNED_CONTEXT ( ( #25221, #29552, #20316 ) ) REPRESENTATION_CONTEXT ( 'NONE', 'WORKASPACE' ) );
#29324=EDGE_CURVE ( 'NONE', #15781, #18049, #24376, .T. ) ;
#29326=CIRCLE ( 'NONE', #14629, 5.000000000000006217 ) ;
#29455=CARTESIAN_POINT ( 'NONE',  ( 8.000000000000010658, 4.618802153517005848, -5.000000000000000888 ) ) ;
#29485=EDGE_CURVE ( 'NONE', #6726, #27863, #27785, .T. ) ;
#29534=ORIENTED_EDGE ( 'NONE', *, *, #14874, .F. ) ;
#29538=CARTESIAN_POINT ( 'NONE',  ( 0.000000000000000000, 0.000000000000000000, 0.000000000000000000 ) ) ;
#29549=CARTESIAN_POINT ( 'NONE',  ( 8.000000000000003553, 4.618802153517037823, -4.285468820183664818 ) ) ;
#29552=( NAMED_UNIT ( * ) PLANE_ANGLE_UNIT ( ) SI_UNIT ( $, .RADIAN. ) );
#29573=EDGE_CURVE ( 'NONE', #6973, #6726, #10607, .T. ) ;
#29627=AXIS2_PLACEMENT_3D ( 'NONE', #639, #15100, #23842 ) ;
#29694=ORIENTED_EDGE ( 'NONE', *, *, #5154, .F. ) ;
#29717=DIRECTION ( 'NONE',  ( 1.000000000000000000, 4.440892098500622217E-16, 0.000000000000000000 ) ) ;
#29818=DIRECTION ( 'NONE',  ( 0.000000000000000000, 0.000000000000000000, 1.000000000000000000 ) ) ;
#29892=CARTESIAN_POINT ( 'NONE',  ( 8.000000000000003553, 4.618802153517037823, -4.285468820183664818 ) ) ;
#29927=EDGE_CURVE ( 'NONE', #14621, #6718, #6358, .T. ) ;
#29936=CARTESIAN_POINT ( 'NONE',  ( -2.644994884459112683, 7.710515798486376582, -4.917753204360280961 ) ) ;
#29949=CARTESIAN_POINT ( 'NONE',  ( -7.372574772901430151E-15, -9.237604307034054330, -5.000000000000000888 ) ) ;
#30047=EDGE_CURVE ( 'NONE', #6624, #24955, #29326, .T. ) ;
#30103=CARTESIAN_POINT ( 'NONE',  ( 0.000000000000000000, 0.000000000000000000, -4.974599999999998801 ) ) ;
#30142=DIRECTION ( 'NONE',  ( 1.000000000000000000, 4.440892098500622217E-16, 0.000000000000000000 ) ) ;
#30232=EDGE_CURVE ( 'NONE', #28625, #8203, #29195, .T. ) ;
ENDSEC;
END-ISO-10303-21;
